ISO-10303-21;
HEADER;
FILE_DESCRIPTION((''),'2;1');
FILE_NAME('Flat_Head_Screw.step','2026-10-09T10:33:02-07:00',(''),(''),'','','');
FILE_SCHEMA (('AUTOMOTIVE_DESIGN { 1 0 10303 214 3 1 1 }'));
ENDSEC;
DATA;
#10=MECHANICAL_DESIGN_GEOMETRIC_PRESENTATION_REPRESENTATION('',(#840),#86330);
#122=ELLIPSE('',#33166,20.5459783090209,1.7907) ;
#123=ELLIPSE('',#33167,20.545978309021,1.7907) ;
#124=ELLIPSE('',#33169,20.545978309021,1.7907) ;
#125=ELLIPSE('',#33170,20.5459783090209,1.7907) ;
#126=ELLIPSE('',#33172,20.545978309021,1.7907) ;
#127=ELLIPSE('',#33173,20.545978309021,1.7907) ;
#128=ELLIPSE('',#33185,20.545978309021,1.7907) ;
#129=ELLIPSE('',#33187,20.545978309021,1.7907) ;
#226=TOROIDAL_SURFACE('',#33146,2.55525626680218,0.0625) ;
#738=(
BOUNDED_SURFACE()
B_SPLINE_SURFACE(1,2,((#49791,#49792,#49793,#49794,#49795,#49796,#49797,
#49798,#49799,#49800,#49801,#49802,#49803,#49804,#49805,#49806,#49807,#49808,
#49809,#49810,#49811,#49812,#49813,#49814,#49815,#49816,#49817,#49818,#49819,
#49820,#49821,#49822,#49823,#49824,#49825,#49826,#49827,#49828,#49829,#49830,
#49831,#49832,#49833,#49834,#49835,#49836,#49837,#49838,#49839,#49840,#49841,
#49842,#49843,#49844,#49845,#49846,#49847,#49848,#49849,#49850,#49851,#49852,
#49853,#49854,#49855,#49856,#49857,#49858,#49859,#49860,#49861,#49862,#49863,
#49864,#49865,#49866,#49867,#49868,#49869,#49870,#49871,#49872,#49873,#49874,
#49875,#49876,#49877,#49878,#49879,#49880,#49881,#49882,#49883,#49884,#49885,
#49886,#49887,#49888,#49889,#49890,#49891,#49892,#49893,#49894,#49895,#49896,
#49897),(#49898,#49899,#49900,#49901,#49902,#49903,#49904,#49905,#49906,
#49907,#49908,#49909,#49910,#49911,#49912,#49913,#49914,#49915,#49916,#49917,
#49918,#49919,#49920,#49921,#49922,#49923,#49924,#49925,#49926,#49927,#49928,
#49929,#49930,#49931,#49932,#49933,#49934,#49935,#49936,#49937,#49938,#49939,
#49940,#49941,#49942,#49943,#49944,#49945,#49946,#49947,#49948,#49949,#49950,
#49951,#49952,#49953,#49954,#49955,#49956,#49957,#49958,#49959,#49960,#49961,
#49962,#49963,#49964,#49965,#49966,#49967,#49968,#49969,#49970,#49971,#49972,
#49973,#49974,#49975,#49976,#49977,#49978,#49979,#49980,#49981,#49982,#49983,
#49984,#49985,#49986,#49987,#49988,#49989,#49990,#49991,#49992,#49993,#49994,
#49995,#49996,#49997,#49998,#49999,#50000,#50001,#50002,#50003,#50004)),
 .UNSPECIFIED.,.F.,.F.,.F.)
B_SPLINE_SURFACE_WITH_KNOTS((2,2),(3,2,2,2,2,2,2,2,2,2,2,2,2,2,2,2,2,2,
2,2,2,2,2,2,2,2,2,2,2,2,2,2,2,2,2,2,2,2,2,2,2,2,2,2,2,2,2,2,2,2,2,2,2,3),
(0.,1.),(0.,0.0185185185185185,0.037037037037037,0.0555555555555556,0.0740740740740741,
0.0925925925925926,0.111111111111111,0.12962962962963,0.148148148148148,
0.166666666666667,0.185185185185185,0.203703703703704,0.222222222222222,
0.240740740740741,0.259259259259259,0.277777777777778,0.296296296296296,
0.314814814814815,0.333333333333333,0.351851851851852,0.37037037037037,
0.388888888888889,0.407407407407407,0.425925925925926,0.444444444444444,
0.462962962962963,0.481481481481481,0.5,0.518518518518518,0.537037037037037,
0.555555555555556,0.574074074074074,0.592592592592593,0.611111111111111,
0.62962962962963,0.648148148148148,0.666666666666667,0.685185185185185,
0.703703703703704,0.722222222222222,0.740740740740741,0.759259259259259,
0.777777777777778,0.796296296296296,0.814814814814815,0.833333333333333,
0.851851851851852,0.87037037037037,0.888888888888889,0.907407407407407,
0.925925925925926,0.944444444444444,0.962962962962963,0.972222222222224),
 .UNSPECIFIED.)
GEOMETRIC_REPRESENTATION_ITEM()
RATIONAL_B_SPLINE_SURFACE(((1.,0.866025403784439,1.,0.866025403784439,1.,
0.866025403784439,1.,0.866025403784439,1.,0.866025403784439,1.,0.866025403784439,
1.,0.866025403784439,1.,0.866025403784439,1.,0.866025403784439,1.,0.866025403784439,
1.,0.866025403784439,1.,0.866025403784439,1.,0.866025403784439,1.,0.866025403784439,
1.,0.866025403784439,1.,0.866025403784439,1.,0.866025403784439,1.,0.866025403784439,
1.,0.866025403784439,1.,0.866025403784439,1.,0.866025403784439,1.,0.866025403784439,
1.,0.866025403784439,1.,0.866025403784439,1.,0.866025403784439,1.,0.866025403784439,
1.,0.866025403784439,1.,0.866025403784439,1.,0.866025403784439,1.,0.866025403784439,
1.,0.866025403784439,1.,0.866025403784439,1.,0.866025403784439,1.,0.866025403784439,
1.,0.866025403784439,1.,0.866025403784439,1.,0.866025403784439,1.,0.866025403784439,
1.,0.866025403784439,1.,0.866025403784439,1.,0.866025403784439,1.,0.866025403784439,
1.,0.866025403784439,1.,0.866025403784439,1.,0.866025403784439,1.,0.866025403784439,
1.,0.866025403784439,1.,0.866025403784439,1.,0.866025403784439,1.,0.866025403784439,
1.,0.866025403784439,1.,0.866025403784439,1.,0.933012701892203,0.933012701892219),
(1.,0.866025403784439,1.,0.866025403784439,1.,0.866025403784439,1.,0.866025403784439,
1.,0.866025403784439,1.,0.866025403784439,1.,0.866025403784439,1.,0.866025403784439,
1.,0.866025403784439,1.,0.866025403784439,1.,0.866025403784439,1.,0.866025403784439,
1.,0.866025403784439,1.,0.866025403784439,1.,0.866025403784439,1.,0.866025403784439,
1.,0.866025403784439,1.,0.866025403784439,1.,0.866025403784439,1.,0.866025403784439,
1.,0.866025403784439,1.,0.866025403784439,1.,0.866025403784439,1.,0.866025403784439,
1.,0.866025403784439,1.,0.866025403784439,1.,0.866025403784439,1.,0.866025403784439,
1.,0.866025403784439,1.,0.866025403784439,1.,0.866025403784439,1.,0.866025403784439,
1.,0.866025403784439,1.,0.866025403784439,1.,0.866025403784439,1.,0.866025403784439,
1.,0.866025403784439,1.,0.866025403784439,1.,0.866025403784439,1.,0.866025403784439,
1.,0.866025403784439,1.,0.866025403784439,1.,0.866025403784439,1.,0.866025403784439,
1.,0.866025403784439,1.,0.866025403784439,1.,0.866025403784439,1.,0.866025403784439,
1.,0.866025403784439,1.,0.866025403784439,1.,0.866025403784439,1.,0.866025403784439,
1.,0.933012701892203,0.933012701892219)))
REPRESENTATION_ITEM('')
SURFACE()
) ;
#739=(
BOUNDED_SURFACE()
B_SPLINE_SURFACE(1,2,((#50005,#50006,#50007,#50008,#50009,#50010,#50011,
#50012,#50013,#50014,#50015,#50016,#50017,#50018,#50019,#50020,#50021,#50022,
#50023,#50024,#50025,#50026,#50027,#50028,#50029,#50030,#50031,#50032,#50033,
#50034,#50035,#50036,#50037,#50038,#50039,#50040,#50041,#50042,#50043,#50044,
#50045,#50046,#50047,#50048,#50049,#50050,#50051,#50052,#50053,#50054,#50055,
#50056,#50057,#50058,#50059,#50060,#50061,#50062,#50063,#50064,#50065,#50066,
#50067,#50068,#50069,#50070,#50071,#50072,#50073,#50074,#50075,#50076,#50077,
#50078,#50079,#50080,#50081,#50082,#50083,#50084,#50085,#50086,#50087,#50088,
#50089,#50090,#50091,#50092,#50093,#50094,#50095,#50096,#50097,#50098,#50099,
#50100,#50101,#50102,#50103,#50104,#50105,#50106,#50107,#50108,#50109,#50110,
#50111),(#50112,#50113,#50114,#50115,#50116,#50117,#50118,#50119,#50120,
#50121,#50122,#50123,#50124,#50125,#50126,#50127,#50128,#50129,#50130,#50131,
#50132,#50133,#50134,#50135,#50136,#50137,#50138,#50139,#50140,#50141,#50142,
#50143,#50144,#50145,#50146,#50147,#50148,#50149,#50150,#50151,#50152,#50153,
#50154,#50155,#50156,#50157,#50158,#50159,#50160,#50161,#50162,#50163,#50164,
#50165,#50166,#50167,#50168,#50169,#50170,#50171,#50172,#50173,#50174,#50175,
#50176,#50177,#50178,#50179,#50180,#50181,#50182,#50183,#50184,#50185,#50186,
#50187,#50188,#50189,#50190,#50191,#50192,#50193,#50194,#50195,#50196,#50197,
#50198,#50199,#50200,#50201,#50202,#50203,#50204,#50205,#50206,#50207,#50208,
#50209,#50210,#50211,#50212,#50213,#50214,#50215,#50216,#50217,#50218)),
 .UNSPECIFIED.,.F.,.F.,.F.)
B_SPLINE_SURFACE_WITH_KNOTS((2,2),(3,2,2,2,2,2,2,2,2,2,2,2,2,2,2,2,2,2,
2,2,2,2,2,2,2,2,2,2,2,2,2,2,2,2,2,2,2,2,2,2,2,2,2,2,2,2,2,2,2,2,2,2,2,3),
(0.,1.),(0.,0.0185185185185185,0.037037037037037,0.0555555555555556,0.0740740740740741,
0.0925925925925926,0.111111111111111,0.12962962962963,0.148148148148148,
0.166666666666667,0.185185185185185,0.203703703703704,0.222222222222222,
0.240740740740741,0.259259259259259,0.277777777777778,0.296296296296296,
0.314814814814815,0.333333333333333,0.351851851851852,0.37037037037037,
0.388888888888889,0.407407407407407,0.425925925925926,0.444444444444444,
0.462962962962963,0.481481481481481,0.5,0.518518518518518,0.537037037037037,
0.555555555555556,0.574074074074074,0.592592592592593,0.611111111111111,
0.62962962962963,0.648148148148148,0.666666666666667,0.685185185185185,
0.703703703703704,0.722222222222222,0.740740740740741,0.759259259259259,
0.777777777777778,0.796296296296296,0.814814814814815,0.833333333333333,
0.851851851851852,0.87037037037037,0.888888888888889,0.907407407407407,
0.925925925925926,0.944444444444444,0.962962962962963,0.972222222222225),
 .UNSPECIFIED.)
GEOMETRIC_REPRESENTATION_ITEM()
RATIONAL_B_SPLINE_SURFACE(((1.,0.866025403784439,1.,0.866025403784439,1.,
0.866025403784439,1.,0.866025403784439,1.,0.866025403784439,1.,0.866025403784439,
1.,0.866025403784439,1.,0.866025403784439,1.,0.866025403784439,1.,0.866025403784439,
1.,0.866025403784439,1.,0.866025403784439,1.,0.866025403784439,1.,0.866025403784439,
1.,0.866025403784439,1.,0.866025403784439,1.,0.866025403784439,1.,0.866025403784439,
1.,0.866025403784439,1.,0.866025403784439,1.,0.866025403784439,1.,0.866025403784439,
1.,0.866025403784439,1.,0.866025403784439,1.,0.866025403784439,1.,0.866025403784439,
1.,0.866025403784439,1.,0.866025403784439,1.,0.866025403784439,1.,0.866025403784439,
1.,0.866025403784439,1.,0.866025403784439,1.,0.866025403784439,1.,0.866025403784439,
1.,0.866025403784439,1.,0.866025403784439,1.,0.866025403784439,1.,0.866025403784439,
1.,0.866025403784439,1.,0.866025403784439,1.,0.866025403784439,1.,0.866025403784439,
1.,0.866025403784439,1.,0.866025403784439,1.,0.866025403784439,1.,0.866025403784439,
1.,0.866025403784439,1.,0.866025403784439,1.,0.866025403784439,1.,0.866025403784439,
1.,0.866025403784439,1.,0.866025403784439,1.,0.933012701892203,0.933012701892219),
(1.,0.866025403784439,1.,0.866025403784439,1.,0.866025403784439,1.,0.866025403784439,
1.,0.866025403784439,1.,0.866025403784439,1.,0.866025403784439,1.,0.866025403784439,
1.,0.866025403784439,1.,0.866025403784439,1.,0.866025403784439,1.,0.866025403784439,
1.,0.866025403784439,1.,0.866025403784439,1.,0.866025403784439,1.,0.866025403784439,
1.,0.866025403784439,1.,0.866025403784439,1.,0.866025403784439,1.,0.866025403784439,
1.,0.866025403784439,1.,0.866025403784439,1.,0.866025403784439,1.,0.866025403784439,
1.,0.866025403784439,1.,0.866025403784439,1.,0.866025403784439,1.,0.866025403784439,
1.,0.866025403784439,1.,0.866025403784439,1.,0.866025403784439,1.,0.866025403784439,
1.,0.866025403784439,1.,0.866025403784439,1.,0.866025403784439,1.,0.866025403784439,
1.,0.866025403784439,1.,0.866025403784439,1.,0.866025403784439,1.,0.866025403784439,
1.,0.866025403784439,1.,0.866025403784439,1.,0.866025403784439,1.,0.866025403784439,
1.,0.866025403784439,1.,0.866025403784439,1.,0.866025403784439,1.,0.866025403784439,
1.,0.866025403784439,1.,0.866025403784439,1.,0.866025403784439,1.,0.866025403784439,
1.,0.933012701892203,0.933012701892219)))
REPRESENTATION_ITEM('')
SURFACE()
) ;
#788=(
BOUNDED_CURVE()
B_SPLINE_CURVE(2,(#49643,#49644,#49645),.UNSPECIFIED.,.F.,.F.)
B_SPLINE_CURVE_WITH_KNOTS((3,3),(-0.0377785531909541,-0.0133078155412431),
 .UNSPECIFIED.)
CURVE()
GEOMETRIC_REPRESENTATION_ITEM()
RATIONAL_B_SPLINE_CURVE((2.38177903497838,1.9561989176297,1.50219886598083))
REPRESENTATION_ITEM('')
) ;
#789=(
BOUNDED_CURVE()
B_SPLINE_CURVE(2,(#49647,#49648,#49649),.UNSPECIFIED.,.F.,.F.)
B_SPLINE_CURVE_WITH_KNOTS((3,3),(0.118635872970107,0.265338602965705),
 .UNSPECIFIED.)
CURVE()
GEOMETRIC_REPRESENTATION_ITEM()
RATIONAL_B_SPLINE_CURVE((2.07975074185157,2.61715986238987,2.83258860692592))
REPRESENTATION_ITEM('')
) ;
#790=(
BOUNDED_CURVE()
B_SPLINE_CURVE(2,(#49651,#49652,#49653),.UNSPECIFIED.,.F.,.F.)
B_SPLINE_CURVE_WITH_KNOTS((3,3),(0.461648610024908,0.608351340026347),
 .UNSPECIFIED.)
CURVE()
GEOMETRIC_REPRESENTATION_ITEM()
RATIONAL_B_SPLINE_CURVE((2.83258860692592,2.61715986238129,2.07975074180877))
REPRESENTATION_ITEM('')
) ;
#791=(
BOUNDED_CURVE()
B_SPLINE_CURVE(2,(#49655,#49656,#49657),.UNSPECIFIED.,.F.,.F.)
B_SPLINE_CURVE_WITH_KNOTS((3,3),(0.770662682377589,0.795133420027306),
 .UNSPECIFIED.)
CURVE()
GEOMETRIC_REPRESENTATION_ITEM()
RATIONAL_B_SPLINE_CURVE((2.38177903497838,1.9561989176296,1.50219886598061))
REPRESENTATION_ITEM('')
) ;
#792=(
BOUNDED_CURVE()
B_SPLINE_CURVE(2,(#49661,#49662,#49663),.UNSPECIFIED.,.F.,.F.)
B_SPLINE_CURVE_WITH_KNOTS((3,3),(-0.037778553190954,-0.0133078155412431),
 .UNSPECIFIED.)
CURVE()
GEOMETRIC_REPRESENTATION_ITEM()
RATIONAL_B_SPLINE_CURVE((2.38177903497838,1.9561989176297,1.50219886598083))
REPRESENTATION_ITEM('')
) ;
#793=(
BOUNDED_CURVE()
B_SPLINE_CURVE(2,(#49665,#49666,#49667),.UNSPECIFIED.,.F.,.F.)
B_SPLINE_CURVE_WITH_KNOTS((3,3),(0.118635872970107,0.265338602965705),
 .UNSPECIFIED.)
CURVE()
GEOMETRIC_REPRESENTATION_ITEM()
RATIONAL_B_SPLINE_CURVE((2.07975074185157,2.61715986238987,2.83258860692592))
REPRESENTATION_ITEM('')
) ;
#794=(
BOUNDED_CURVE()
B_SPLINE_CURVE(2,(#49669,#49670,#49671),.UNSPECIFIED.,.F.,.F.)
B_SPLINE_CURVE_WITH_KNOTS((3,3),(0.461648610024907,0.608351340026346),
 .UNSPECIFIED.)
CURVE()
GEOMETRIC_REPRESENTATION_ITEM()
RATIONAL_B_SPLINE_CURVE((2.83258860692591,2.61715986238129,2.07975074180877))
REPRESENTATION_ITEM('')
) ;
#795=(
BOUNDED_CURVE()
B_SPLINE_CURVE(2,(#49673,#49674,#49675),.UNSPECIFIED.,.F.,.F.)
B_SPLINE_CURVE_WITH_KNOTS((3,3),(0.770662682377589,0.795133420027306),
 .UNSPECIFIED.)
CURVE()
GEOMETRIC_REPRESENTATION_ITEM()
RATIONAL_B_SPLINE_CURVE((2.38177903497839,1.95619891762961,1.50219886598062))
REPRESENTATION_ITEM('')
) ;
#796=(
BOUNDED_CURVE()
B_SPLINE_CURVE(2,(#49679,#49680,#49681),.UNSPECIFIED.,.F.,.F.)
B_SPLINE_CURVE_WITH_KNOTS((3,3),(0.77066268237759,0.795133420027307),
 .UNSPECIFIED.)
CURVE()
GEOMETRIC_REPRESENTATION_ITEM()
RATIONAL_B_SPLINE_CURVE((2.38177903497836,1.95619891762959,1.5021988659806))
REPRESENTATION_ITEM('')
) ;
#797=(
BOUNDED_CURVE()
B_SPLINE_CURVE(2,(#49683,#49684,#49685),.UNSPECIFIED.,.F.,.F.)
B_SPLINE_CURVE_WITH_KNOTS((3,3),(-0.608351340026346,-0.461648610024908),
 .UNSPECIFIED.)
CURVE()
GEOMETRIC_REPRESENTATION_ITEM()
RATIONAL_B_SPLINE_CURVE((2.07975074180878,2.61715986238129,2.83258860692592))
REPRESENTATION_ITEM('')
) ;
#798=(
BOUNDED_CURVE()
B_SPLINE_CURVE(2,(#49687,#49688,#49689),.UNSPECIFIED.,.F.,.F.)
B_SPLINE_CURVE_WITH_KNOTS((3,3),(-0.265338602965705,-0.118635872970107),
 .UNSPECIFIED.)
CURVE()
GEOMETRIC_REPRESENTATION_ITEM()
RATIONAL_B_SPLINE_CURVE((2.83258860692592,2.61715986238987,2.07975074185157))
REPRESENTATION_ITEM('')
) ;
#799=(
BOUNDED_CURVE()
B_SPLINE_CURVE(2,(#49691,#49692,#49693),.UNSPECIFIED.,.F.,.F.)
B_SPLINE_CURVE_WITH_KNOTS((3,3),(-0.0377785531909541,-0.0133078155412431),
 .UNSPECIFIED.)
CURVE()
GEOMETRIC_REPRESENTATION_ITEM()
RATIONAL_B_SPLINE_CURVE((2.38177903497838,1.9561989176297,1.50219886598083))
REPRESENTATION_ITEM('')
) ;
#800=(
BOUNDED_CURVE()
B_SPLINE_CURVE(2,(#49697,#49698,#49699),.UNSPECIFIED.,.F.,.F.)
B_SPLINE_CURVE_WITH_KNOTS((3,3),(0.770662682377589,0.795133420027306),
 .UNSPECIFIED.)
CURVE()
GEOMETRIC_REPRESENTATION_ITEM()
RATIONAL_B_SPLINE_CURVE((2.38177903497838,1.9561989176296,1.50219886598061))
REPRESENTATION_ITEM('')
) ;
#801=(
BOUNDED_CURVE()
B_SPLINE_CURVE(2,(#49701,#49702,#49703),.UNSPECIFIED.,.F.,.F.)
B_SPLINE_CURVE_WITH_KNOTS((3,3),(-0.608351340026346,-0.461648610024906),
 .UNSPECIFIED.)
CURVE()
GEOMETRIC_REPRESENTATION_ITEM()
RATIONAL_B_SPLINE_CURVE((2.07975074180877,2.61715986238129,2.83258860692592))
REPRESENTATION_ITEM('')
) ;
#802=(
BOUNDED_CURVE()
B_SPLINE_CURVE(2,(#49705,#49706,#49707),.UNSPECIFIED.,.F.,.F.)
B_SPLINE_CURVE_WITH_KNOTS((3,3),(-0.265338602965706,-0.118635872970107),
 .UNSPECIFIED.)
CURVE()
GEOMETRIC_REPRESENTATION_ITEM()
RATIONAL_B_SPLINE_CURVE((2.83258860692592,2.61715986238987,2.07975074185157))
REPRESENTATION_ITEM('')
) ;
#803=(
BOUNDED_CURVE()
B_SPLINE_CURVE(2,(#49709,#49710,#49711),.UNSPECIFIED.,.F.,.F.)
B_SPLINE_CURVE_WITH_KNOTS((3,3),(-0.0377785531909542,-0.0133078155412432),
 .UNSPECIFIED.)
CURVE()
GEOMETRIC_REPRESENTATION_ITEM()
RATIONAL_B_SPLINE_CURVE((2.38177903497838,1.95619891762971,1.50219886598083))
REPRESENTATION_ITEM('')
) ;
#816=SHAPE_REPRESENTATION_RELATIONSHIP('SRR','None',#86458,#828) ;
#828=ADVANCED_BREP_SHAPE_REPRESENTATION('',(#852),#86312) ;
#840=STYLED_ITEM('',(#86582),#852) ;
#852=MANIFOLD_SOLID_BREP('Body1',#32639) ;
#880=CONICAL_SURFACE('',#33151,1.4224,0.715584993317677) ;
#881=CONICAL_SURFACE('',#33157,0.92075,0.78539816339745) ;
#882=CONICAL_SURFACE('',#33159,0.968718914342085,0.715584993317677) ;
#1050=FACE_BOUND('',#4391,.T.) ;
#1226=B_SPLINE_CURVE_WITH_KNOTS('',3,(#48641,#48642,#48643,#48644,#48645,
#48646),.UNSPECIFIED.,.F.,.F.,(4,2,4),(3.76031917570416,3.76804109815423,
3.80554677388846),.UNSPECIFIED.) ;
#1227=B_SPLINE_CURVE_WITH_KNOTS('',3,(#48652,#48653,#48654,#48655,#48656,
#48657,#48658,#48659,#48660,#48661,#48662,#48663,#48664,#48665,#48666,#48667,
#48668,#48669,#48670,#48671,#48672,#48673,#48674,#48675,#48676,#48677,#48678,
#48679,#48680,#48681,#48682,#48683,#48684,#48685,#48686,#48687),
 .UNSPECIFIED.,.F.,.F.,(4,2,2,2,2,2,2,2,2,2,2,2,2,2,2,2,2,4),(3.1176227748347,
3.13096592162681,3.17214416512159,3.21178089063607,3.25164155415437,3.29229454274865,
3.331416941854,3.37209007584933,3.41210537289544,3.45097921650868,3.49166209479253,
3.5312435182945,3.57078165411375,3.61138931078773,3.65047051941298,3.69142496434553,
3.73140528845282,3.76031917570416),.UNSPECIFIED.) ;
#1228=B_SPLINE_CURVE_WITH_KNOTS('',3,(#48690,#48691,#48692,#48693,#48694,
#48695,#48696,#48697,#48698,#48699,#48700,#48701,#48702,#48703,#48704,#48705,
#48706,#48707,#48708,#48709,#48710,#48711,#48712,#48713,#48714,#48715,#48716,
#48717,#48718,#48719,#48720,#48721,#48722,#48723),.UNSPECIFIED.,.F.,.F.,
(4,2,2,2,2,2,2,2,2,2,2,2,2,2,2,2,4),(0.,0.0362447607018933,0.0713825393809272,
0.110374339020624,0.150892059768638,0.190667140095241,0.230173971071058,
0.271217309410474,0.310173121012165,0.350138836987173,0.390769526483312,
0.429629582897894,0.469935119533493,0.509766123742405,0.549077933529619,
0.589919103429393,0.605457920328374),.UNSPECIFIED.) ;
#1229=B_SPLINE_CURVE_WITH_KNOTS('',3,(#48728,#48729,#48730,#48731,#48732,
#48733,#48734,#48735,#48736,#48737,#48738,#48739,#48740,#48741,#48742,#48743,
#48744,#48745,#48746,#48747,#48748,#48749,#48750,#48751,#48752,#48753,#48754,
#48755,#48756,#48757,#48758,#48759,#48760,#48761,#48762,#48763),
 .UNSPECIFIED.,.F.,.F.,(4,2,2,2,2,2,2,2,2,2,2,2,2,2,2,2,2,4),(2.47551363283054,
2.49265917852922,2.53346259133496,2.57273744940686,2.6127542482078,2.6530100280249,
2.6918288302763,2.73245659923037,2.77235334434581,2.81134989267037,2.85231605851498,
2.89174829275779,2.93165078035237,2.9720823268742,3.01106427522818,3.05181132055974,
3.09190687687269,3.1176227748347),.UNSPECIFIED.) ;
#1230=B_SPLINE_CURVE_WITH_KNOTS('',3,(#48764,#48765,#48766,#48767,#48768,
#48769,#48770,#48771,#48772,#48773,#48774,#48775,#48776,#48777,#48778,#48779,
#48780,#48781,#48782,#48783,#48784,#48785,#48786,#48787,#48788,#48789,#48790,
#48791,#48792,#48793,#48794,#48795,#48796,#48797,#48798,#48799),
 .UNSPECIFIED.,.F.,.F.,(4,2,2,2,2,2,2,2,2,2,2,2,2,2,2,2,2,4),(0.605457920328374,
0.62882567261221,0.668602087446539,0.709123355352179,0.747832945812351,
0.787971715930476,0.827929939366068,0.867093635478729,0.907781744119965,
0.946706186283578,0.986340613635276,1.0268012450227,1.06542475571967,1.10544143735414,
1.14559125591013,1.18465312778227,1.22523661095565,1.24467539849028),
 .UNSPECIFIED.) ;
#1231=B_SPLINE_CURVE_WITH_KNOTS('',3,(#48804,#48805,#48806,#48807,#48808,
#48809,#48810,#48811,#48812,#48813,#48814,#48815,#48816,#48817,#48818,#48819,
#48820,#48821,#48822,#48823,#48824,#48825,#48826,#48827,#48828,#48829,#48830,
#48831,#48832,#48833,#48834,#48835,#48836,#48837,#48838,#48839),
 .UNSPECIFIED.,.F.,.F.,(4,2,2,2,2,2,2,2,2,2,2,2,2,2,2,2,2,4),(1.83528891850249,
1.85722847759532,1.8969538274905,1.93605280977056,1.97648770036395,2.01652614280508,
2.05521120838619,2.09574601251688,2.13538722021168,2.17445838474558,2.21514772520206,
2.25431172318189,2.29450885496653,2.33463376922292,2.37335404255371,2.41391189247215,
2.45365730428937,2.47551363283054),.UNSPECIFIED.) ;
#1232=B_SPLINE_CURVE_WITH_KNOTS('',3,(#48840,#48841,#48842,#48843,#48844,
#48845,#48846,#48847,#48848,#48849,#48850,#48851,#48852,#48853,#48854,#48855,
#48856,#48857,#48858,#48859,#48860,#48861,#48862,#48863,#48864,#48865,#48866,
#48867,#48868,#48869,#48870,#48871,#48872,#48873,#48874,#48875),
 .UNSPECIFIED.,.F.,.F.,(4,2,2,2,2,2,2,2,2,2,2,2,2,2,2,2,2,4),(1.24467539849028,
1.26424176879834,1.30378115879747,1.34422744626993,1.38282758397962,1.42276641203434,
1.46316332143799,1.50216897752343,1.54269549810761,1.58184036229905,1.62133120061554,
1.66180699594723,1.70044290755449,1.74034782923514,1.78103747545853,1.82003173152049,
1.86054803985681,1.88375019029688),.UNSPECIFIED.) ;
#1233=B_SPLINE_CURVE_WITH_KNOTS('',3,(#48880,#48881,#48882,#48883,#48884,
#48885,#48886,#48887,#48888,#48889,#48890,#48891,#48892,#48893,#48894,#48895,
#48896,#48897,#48898,#48899,#48900,#48901,#48902,#48903,#48904,#48905,#48906,
#48907,#48908,#48909,#48910,#48911,#48912,#48913,#48914,#48915),
 .UNSPECIFIED.,.F.,.F.,(4,2,2,2,2,2,2,2,2,2,2,2,2,2,2,2,2,4),(1.19352210642917,
1.21931788538152,1.25939797995323,1.30012516537162,1.33909103063952,1.37950565671438,
1.41937748903333,1.45879257698243,1.49974090167009,1.53871284696102,1.57859183853036,
1.61919725112725,1.65799679236964,1.69823346376681,1.73821597445172,1.77747140610762,
1.81825458942883,1.83528891850249),.UNSPECIFIED.) ;
#1234=B_SPLINE_CURVE_WITH_KNOTS('',3,(#48916,#48917,#48918,#48919,#48920,
#48921,#48922,#48923,#48924,#48925,#48926,#48927,#48928,#48929,#48930,#48931,
#48932,#48933,#48934,#48935,#48936,#48937,#48938,#48939,#48940,#48941,#48942,
#48943,#48944,#48945,#48946,#48947,#48948,#48949,#48950,#48951),
 .UNSPECIFIED.,.F.,.F.,(4,2,2,2,2,2,2,2,2,2,2,2,2,2,2,2,2,4),(1.88375019029688,
1.89988198230334,1.94067697355692,1.97994413167152,2.0198125107436,2.0600679972603,
2.0988807154181,2.13947841767806,2.17938687755795,2.218325919683,2.25930801187248,
2.29875579904418,2.33854583410525,2.37899954199203,2.41792903125738,2.45842422439584,
2.49823169141323,2.52462983086155),.UNSPECIFIED.) ;
#1235=B_SPLINE_CURVE_WITH_KNOTS('',3,(#48956,#48957,#48958,#48959,#48960,
#48961,#48962,#48963,#48964,#48965,#48966,#48967,#48968,#48969,#48970,#48971,
#48972,#48973,#48974,#48975,#48976,#48977,#48978,#48979,#48980,#48981,#48982,
#48983,#48984,#48985,#48986,#48987,#48988,#48989,#48990,#48991),
 .UNSPECIFIED.,.F.,.F.,(4,2,2,2,2,2,2,2,2,2,2,2,2,2,2,2,2,4),(0.551086143700849,
0.580091364104038,0.620060698665072,0.660986348613251,0.700055552534506,
0.74065064044146,0.780165727193365,0.819734488707212,0.860400666874468,
0.899256714752227,0.939258647894076,0.9799148702805,1.01902321382585,1.05966148145784,
1.09949533248928,1.13911718679827,1.18027997197713,1.19352210642917),
 .UNSPECIFIED.) ;
#1236=B_SPLINE_CURVE_WITH_KNOTS('',3,(#48992,#48993,#48994,#48995,#48996,
#48997,#48998,#48999,#49000,#49001,#49002,#49003,#49004,#49005,#49006,#49007,
#49008,#49009,#49010,#49011,#49012,#49013,#49014,#49015,#49016,#49017,#49018,
#49019,#49020,#49021,#49022,#49023,#49024,#49025,#49026,#49027),
 .UNSPECIFIED.,.F.,.F.,(4,2,2,2,2,2,2,2,2,2,2,2,2,2,2,2,2,4),(2.52462983086155,
2.53695341089861,2.57783997991567,2.61719599397139,2.6566618302656,2.69703185339974,
2.73588298516227,2.77625185641937,2.81599906562349,2.85456780715886,2.8949483004276,
2.93427001044845,2.97345040080917,3.01379553906095,3.05262495156429,3.09316170023457,
3.13289646793589,3.16251647559856),.UNSPECIFIED.) ;
#1237=B_SPLINE_CURVE_WITH_KNOTS('',3,(#49033,#49034,#49035,#49036,#49037,
#49038,#49039,#49040,#49041,#49042,#49043,#49044,#49045,#49046,#49047,#49048,
#49049,#49050,#49051,#49052,#49053,#49054),.UNSPECIFIED.,.F.,.F.,(4,2,2,
2,2,2,2,2,2,2,4),(-0.5127490185938,-0.4791046818415,-0.422350585875431,
-0.367729891266528,-0.310500088892541,-0.254538834991981,-0.200332174033985,
-0.143564859003832,-0.0882110501729356,-0.0448733995117723,-9.99999997697287E-7),
 .UNSPECIFIED.) ;
#1238=B_SPLINE_CURVE_WITH_KNOTS('',3,(#49064,#49065,#49066,#49067,#49068,
#49069,#49070,#49071,#49072,#49073,#49074,#49075,#49076,#49077,#49078,#49079,
#49080,#49081),.UNSPECIFIED.,.F.,.F.,(4,2,2,2,2,2,2,2,4),(-4.73647368332327,
-4.69196976536075,-4.64843188712961,-4.59433805239982,-4.53841454670932,
-4.4815415422272,-4.42697305731884,-4.37027094054635,-4.33840784589812),
 .UNSPECIFIED.) ;
#1239=B_SPLINE_CURVE_WITH_KNOTS('',3,(#49086,#49087,#49088,#49089,#49090,
#49091,#49092,#49093,#49094,#49095,#49096,#49097,#49098,#49099,#49100,#49101,
#49102,#49103,#49104,#49105,#49106,#49107,#49108,#49109,#49110,#49111,#49112,
#49113,#49114,#49115,#49116,#49117,#49118,#49119,#49120,#49121),
 .UNSPECIFIED.,.F.,.F.,(4,2,2,2,2,2,2,2,2,2,2,2,2,2,2,2,2,4),(-1.4130436997725,
-1.37120186134835,-1.31475362738297,-1.26035723096277,-1.20347805742769,
-1.14760499381641,-1.09307418860522,-1.03566282562664,-0.980432459772098,
-0.924723619832426,-0.868039151939393,-0.813480696262236,-0.756668230447416,
-0.700772408702761,-0.646451202546037,-0.589621104290089,-0.534341469973269,
-0.5127490185938),.UNSPECIFIED.) ;
#1240=B_SPLINE_CURVE_WITH_KNOTS('',3,(#49122,#49123,#49124,#49125,#49126,
#49127,#49128,#49129,#49130,#49131,#49132,#49133,#49134,#49135,#49136,#49137,
#49138,#49139,#49140,#49141,#49142,#49143,#49144,#49145,#49146,#49147,#49148,
#49149,#49150,#49151,#49152,#49153,#49154,#49155,#49156,#49157),
 .UNSPECIFIED.,.F.,.F.,(4,2,2,2,2,2,2,2,2,2,2,2,2,2,2,2,2,4),(-4.33840784589812,
-4.31528370261049,-4.26006124925725,-4.2033565108894,-4.14918639075426,
-4.09335286929486,-4.03666354972709,-3.98217463220581,-3.92556044694046,
-3.87015538869561,-3.81500178242087,-3.75766624363665,-3.70333313608232,
-3.64753965093067,-3.59081629313595,-3.53651544329802,-3.48015656427228,
-3.44034153207722),.UNSPECIFIED.) ;
#1241=B_SPLINE_CURVE_WITH_KNOTS('',3,(#49162,#49163,#49164,#49165,#49166,
#49167,#49168,#49169,#49170,#49171,#49172,#49173,#49174,#49175,#49176,#49177,
#49178,#49179,#49180,#49181,#49182,#49183,#49184,#49185,#49186,#49187,#49188,
#49189,#49190,#49191,#49192,#49193,#49194,#49195,#49196,#49197),
 .UNSPECIFIED.,.F.,.F.,(4,2,2,2,2,2,2,2,2,2,2,2,2,2,2,2,2,4),(-2.3125340189891,
-2.26280853691107,-2.20670330818657,-2.15246510273515,-2.09565008652731,
-2.04014590130349,-1.98534363457005,-1.92833595983324,-1.87348000641213,
-1.81705543445323,-1.76080108846584,-1.70653159540569,-1.64970741813391,
-1.59404239838814,-1.53942370358624,-1.48223832446272,-1.42721794334907,
-1.4130436997725),.UNSPECIFIED.) ;
#1242=B_SPLINE_CURVE_WITH_KNOTS('',3,(#49198,#49199,#49200,#49201,#49202,
#49203,#49204,#49205,#49206,#49207,#49208,#49209,#49210,#49211,#49212,#49213,
#49214,#49215,#49216,#49217,#49218,#49219,#49220,#49221,#49222,#49223,#49224,
#49225,#49226,#49227,#49228,#49229,#49230,#49231,#49232,#49233),
 .UNSPECIFIED.,.F.,.F.,(4,2,2,2,2,2,2,2,2,2,2,2,2,2,2,2,2,4),(-3.44034153207722,
-3.42449939324888,-3.3695764327963,-3.31248866822477,-3.25811683401008,
-3.20255259965505,-3.14590743519229,-3.09177932604525,-3.03563435486918,
-2.97961691515219,-2.92488004954696,-2.8679929655988,-2.81348320940942,
-2.75810237416364,-2.70148807555117,-2.64743700528058,-2.59146262196782,
-2.54379457940395),.UNSPECIFIED.) ;
#1243=B_SPLINE_CURVE_WITH_KNOTS('',3,(#49238,#49239,#49240,#49241,#49242,
#49243,#49244,#49245,#49246,#49247,#49248,#49249,#49250,#49251,#49252,#49253,
#49254,#49255,#49256,#49257,#49258,#49259,#49260,#49261,#49262,#49263,#49264,
#49265,#49266,#49267,#49268,#49269,#49270,#49271,#49272,#49273,#49274,#49275),
 .UNSPECIFIED.,.F.,.F.,(4,2,2,2,2,2,2,2,2,2,2,2,2,2,2,2,2,2,4),(-3.21306377665209,
-3.2109350187238,-3.15630999768433,-3.09955495100989,-3.04394942532879,
-2.98865641028171,-2.93117704806814,-2.87667453878721,-2.82073950424026,
-2.7638518318754,-2.70940943883827,-2.65290505018767,-2.59703151900695,
-2.54196402257734,-2.48472704457828,-2.43017216514208,-2.37446111862928,
-2.31972208641484,-2.3125340189891),.UNSPECIFIED.) ;
#1244=B_SPLINE_CURVE_WITH_KNOTS('',3,(#49276,#49277,#49278,#49279,#49280,
#49281,#49282,#49283,#49284,#49285,#49286,#49287,#49288,#49289,#49290,#49291,
#49292,#49293,#49294,#49295,#49296,#49297,#49298,#49299,#49300,#49301,#49302,
#49303,#49304,#49305,#49306,#49307,#49308,#49309,#49310,#49311),
 .UNSPECIFIED.,.F.,.F.,(4,2,2,2,2,2,2,2,2,2,2,2,2,2,2,2,2,4),(-2.54379457940395,
-2.53499384249712,-2.48039669454153,-2.42366105417301,-2.36892283947657,
-2.31203709403285,-2.2573015005488,-2.20128396827585,-2.14514036297612,
-2.09101342368331,-2.03436929753395,-1.9788064537663,-1.92443527467436,
-1.86734896827102,-1.81242739278087,-1.75677036765928,-1.7004129599865,
-1.64704707967164),.UNSPECIFIED.) ;
#1245=B_SPLINE_CURVE_WITH_KNOTS('',3,(#49316,#49317,#49318,#49319,#49320,
#49321,#49322,#49323,#49324,#49325,#49326,#49327,#49328,#49329,#49330,#49331,
#49332,#49333,#49334,#49335,#49336,#49337,#49338,#49339,#49340,#49341,#49342,
#49343,#49344,#49345,#49346,#49347,#49348,#49349,#49350,#49351),
 .UNSPECIFIED.,.F.,.F.,(4,2,2,2,2,2,2,2,2,2,2,2,2,2,2,2,2,4),(-4.11267130303842,
-4.10328051065977,-4.04848046904968,-3.99153304600001,-3.93665386620444,
-3.88120392580031,-3.82439128324491,-3.770151349457,-3.71409683652575,-3.65700590541931,
-3.60230555473109,-3.54546704580972,-3.49029481285965,-3.43493792993847,
-3.37807712349796,-3.32375037552931,-3.2677797079742,-3.21306377665209),
 .UNSPECIFIED.) ;
#1246=B_SPLINE_CURVE_WITH_KNOTS('',3,(#49352,#49353,#49354,#49355,#49356,
#49357,#49358,#49359,#49360,#49361,#49362,#49363,#49364,#49365,#49366,#49367,
#49368,#49369,#49370,#49371,#49372,#49373,#49374,#49375,#49376,#49377,#49378,
#49379,#49380,#49381,#49382,#49383,#49384,#49385,#49386,#49387,#49388,#49389),
 .UNSPECIFIED.,.F.,.F.,(4,2,2,2,2,2,2,2,2,2,2,2,2,2,2,2,2,2,4),(-1.64704707967164,
-1.64611351156563,-1.58939131209299,-1.53359932931609,-1.47926712186125,
-1.42193315673438,-1.36678104496521,-1.31137640384191,-1.25476379265969,
-1.20027638045271,-1.14358837833567,-1.08775644043887,-1.03358743775143,
-0.976884004990081,-0.92166313991216,-0.866676489253686,-0.809975892999753,
-0.755408860368642,-0.748981824776657),.UNSPECIFIED.) ;
#1247=B_SPLINE_CURVE_WITH_KNOTS('',3,(#49392,#49393,#49394,#49395,#49396,
#49397,#49398,#49399,#49400,#49401,#49402,#49403,#49404,#49405,#49406,#49407,
#49408,#49409,#49410,#49411,#49412,#49413,#49414,#49415,#49416,#49417,#49418,
#49419,#49420,#49421),.UNSPECIFIED.,.F.,.F.,(4,2,2,2,2,2,2,2,2,2,2,2,2,
2,4),(-0.748981824776657,-0.698535993165537,-0.642614124209802,-0.588521531236234,
-0.531860990174686,-0.476540820790738,-0.421837810676442,-0.365022008689484,
-0.310349358314276,-0.253978727958169,-0.197918590589397,-0.143815584116504,
-0.0871557349535602,-0.04281124218475,-9.99999995254797E-7),
 .UNSPECIFIED.) ;
#1248=B_SPLINE_CURVE_WITH_KNOTS('',3,(#49424,#49425,#49426,#49427,#49428,
#49429,#49430,#49431,#49432,#49433,#49434,#49435,#49436,#49437,#49438,#49439,
#49440,#49441,#49442,#49443,#49444,#49445,#49446,#49447,#49448,#49449),
 .UNSPECIFIED.,.F.,.F.,(4,2,2,2,2,2,2,2,2,2,2,2,4),(-4.75229088586126,-4.70738064000878,
-4.66190994418552,-4.60554452353605,-4.54940449410308,-4.49445665866338,
-4.43734919801762,-4.38268536498262,-4.32709195636778,-4.27028565227991,
-4.2160470765991,-4.15986005312993,-4.11267130303842),.UNSPECIFIED.) ;
#1249=B_SPLINE_CURVE_WITH_KNOTS('',3,(#49452,#49453,#49454,#49455,#49456,
#49457,#49458,#49459,#49460,#49461,#49462,#49463,#49464,#49465,#49466,#49467,
#49468,#49469,#49470,#49471,#49472,#49473,#49474,#49475,#49476,#49477,#49478,
#49479,#49480,#49481,#49482,#49483,#49484,#49485,#49486,#49487),
 .UNSPECIFIED.,.F.,.F.,(4,2,2,2,2,2,2,2,2,2,2,2,2,2,2,2,2,4),(3.16251647559856,
3.17137245211693,3.2116796469811,3.25100123675646,3.28999047999364,3.33034285308588,
3.36918080157474,3.40942349288676,3.44918923883973,3.48762599981309,3.52790110502513,
3.56726810641456,3.60611479764238,3.64652089125254,3.68541194336664,3.72540539515703,
3.75694807253539,3.78793834700464),.UNSPECIFIED.) ;
#1250=B_SPLINE_CURVE_WITH_KNOTS('',3,(#49490,#49491,#49492,#49493,#49494,
#49495,#49496,#49497,#49498,#49499,#49500,#49501,#49502,#49503,#49504,#49505,
#49506,#49507,#49508,#49509,#49510,#49511,#49512,#49513,#49514,#49515,#49516,
#49517,#49518,#49519,#49520,#49521),.UNSPECIFIED.,.F.,.F.,(4,2,2,2,2,2,
2,2,2,2,2,2,2,2,2,4),(0.,0.0310342811770257,0.0631788586655503,0.103792072582309,
0.142927747157277,0.182499758214421,0.223021898301352,0.26169644603923,
0.301676590400516,0.34228887040074,0.381346179193425,0.421927213271208,
0.461229947766521,0.50077767437492,0.541351637872867,0.551086143700849),
 .UNSPECIFIED.) ;
#1251=B_SPLINE_CURVE_WITH_KNOTS('',3,(#49575,#49576,#49577,#49578,#49579,
#49580,#49581,#49582,#49583,#49584,#49585,#49586,#49587,#49588,#49589,#49590,
#49591,#49592,#49593,#49594,#49595,#49596,#49597,#49598,#49599,#49600,#49601,
#49602),.UNSPECIFIED.,.F.,.F.,(4,2,2,2,2,2,2,2,2,2,2,2,2,4),(0.399647517238767,
0.414836450199711,0.509002403599096,0.597571527890476,0.712371649335664,
0.853837527204609,1.00187230702159,1.07695219700279,1.22621700116326,1.38697607123365,
1.59961645957477,1.92493151906482,2.10597394645267,2.30088796086391),
 .UNSPECIFIED.) ;
#1252=B_SPLINE_CURVE_WITH_KNOTS('',3,(#49606,#49607,#49608,#49609,#49610,
#49611,#49612,#49613,#49614,#49615,#49616,#49617,#49618,#49619,#49620,#49621),
 .UNSPECIFIED.,.F.,.F.,(4,2,2,2,2,2,2,4),(0.,0.0370319719196131,0.0786050619190432,
0.13215361237448,0.200684934374393,0.287669832057025,0.368937178455222,
0.399647517238767),.UNSPECIFIED.) ;
#1253=B_SPLINE_CURVE_WITH_KNOTS('',3,(#49622,#49623,#49624,#49625,#49626,
#49627,#49628,#49629,#49630,#49631,#49632,#49633,#49634,#49635),
 .UNSPECIFIED.,.F.,.F.,(4,2,2,2,2,2,4),(-0.43561391109166,-0.34804890840793,
-0.259297090185586,-0.130480653501234,-0.0941897273832555,-0.0477567516765395,
-1.00000015618162E-6),.UNSPECIFIED.) ;
#1254=B_SPLINE_CURVE_WITH_KNOTS('',3,(#49754,#49755,#49756,#49757,#49758,
#49759,#49760,#49761,#49762,#49763,#49764,#49765,#49766,#49767,#49768,#49769,
#49770,#49771),.UNSPECIFIED.,.F.,.F.,(4,2,2,2,2,2,2,2,4),(-0.187329172980139,
-0.147618547087121,-0.107318887539879,-0.0863692505416251,-0.0717625756301755,
-0.064857392647619,-0.0552393980697806,-0.026417184758918,0.),
 .UNSPECIFIED.) ;
#1255=B_SPLINE_CURVE_WITH_KNOTS('',3,(#49772,#49773,#49774,#49775,#49776,
#49777,#49778,#49779,#49780,#49781,#49782,#49783,#49784,#49785,#49786,#49787,
#49788,#49789),.UNSPECIFIED.,.F.,.F.,(4,2,2,2,2,2,2,2,4),(-0.248177093231301,
-0.207320659555912,-0.163004039773727,-0.146139995385165,-0.120240458034777,
-0.0958299418542064,-0.0607027452784435,-0.0303308437384981,-1.00000010200274E-6),
 .UNSPECIFIED.) ;
#1760=PLANE('',#33152) ;
#1761=PLANE('',#33174) ;
#1762=PLANE('',#33175) ;
#1763=PLANE('',#33176) ;
#1764=PLANE('',#33177) ;
#1765=PLANE('',#33178) ;
#1766=PLANE('',#33179) ;
#1767=PLANE('',#33180) ;
#1768=PLANE('',#33181) ;
#1769=PLANE('',#33182) ;
#1770=PLANE('',#33183) ;
#1771=PLANE('',#33184) ;
#1772=PLANE('',#33188) ;
#1773=PLANE('',#33189) ;
#1774=PLANE('',#33190) ;
#1775=PLANE('',#33191) ;
#1776=PLANE('',#33192) ;
#1777=PLANE('',#33193) ;
#1778=PLANE('',#33194) ;
#2437=FACE_OUTER_BOUND('',#4375,.T.) ;
#2438=FACE_OUTER_BOUND('',#4376,.T.) ;
#2439=FACE_OUTER_BOUND('',#4377,.T.) ;
#2440=FACE_OUTER_BOUND('',#4378,.T.) ;
#2441=FACE_OUTER_BOUND('',#4379,.T.) ;
#2442=FACE_OUTER_BOUND('',#4380,.T.) ;
#2443=FACE_OUTER_BOUND('',#4381,.T.) ;
#2444=FACE_OUTER_BOUND('',#4382,.T.) ;
#2445=FACE_OUTER_BOUND('',#4383,.T.) ;
#2446=FACE_OUTER_BOUND('',#4384,.T.) ;
#2447=FACE_OUTER_BOUND('',#4385,.T.) ;
#2448=FACE_OUTER_BOUND('',#4386,.T.) ;
#2449=FACE_OUTER_BOUND('',#4387,.T.) ;
#2450=FACE_OUTER_BOUND('',#4388,.T.) ;
#2451=FACE_OUTER_BOUND('',#4389,.T.) ;
#2452=FACE_OUTER_BOUND('',#4390,.T.) ;
#2453=FACE_OUTER_BOUND('',#4392,.T.) ;
#2454=FACE_OUTER_BOUND('',#4393,.T.) ;
#2455=FACE_OUTER_BOUND('',#4394,.T.) ;
#2456=FACE_OUTER_BOUND('',#4395,.T.) ;
#2457=FACE_OUTER_BOUND('',#4396,.T.) ;
#2458=FACE_OUTER_BOUND('',#4397,.T.) ;
#2459=FACE_OUTER_BOUND('',#4398,.T.) ;
#2460=FACE_OUTER_BOUND('',#4399,.T.) ;
#2461=FACE_OUTER_BOUND('',#4400,.T.) ;
#2462=FACE_OUTER_BOUND('',#4401,.T.) ;
#2463=FACE_OUTER_BOUND('',#4402,.T.) ;
#2464=FACE_OUTER_BOUND('',#4403,.T.) ;
#2465=FACE_OUTER_BOUND('',#4404,.T.) ;
#2466=FACE_OUTER_BOUND('',#4405,.T.) ;
#2467=FACE_OUTER_BOUND('',#4406,.T.) ;
#2468=FACE_OUTER_BOUND('',#4407,.T.) ;
#2469=FACE_OUTER_BOUND('',#4408,.T.) ;
#2470=FACE_OUTER_BOUND('',#4409,.T.) ;
#2471=FACE_OUTER_BOUND('',#4410,.T.) ;
#2472=FACE_OUTER_BOUND('',#4411,.T.) ;
#2473=FACE_OUTER_BOUND('',#4412,.T.) ;
#2474=FACE_OUTER_BOUND('',#4413,.T.) ;
#2475=FACE_OUTER_BOUND('',#4414,.T.) ;
#2476=FACE_OUTER_BOUND('',#4415,.T.) ;
#2477=FACE_OUTER_BOUND('',#4416,.T.) ;
#2478=FACE_OUTER_BOUND('',#4417,.T.) ;
#4375=EDGE_LOOP('',(#21312,#21313,#21314)) ;
#4376=EDGE_LOOP('',(#21315,#21316,#21317,#21318,#21319)) ;
#4377=EDGE_LOOP('',(#21320,#21321,#21322,#21323)) ;
#4378=EDGE_LOOP('',(#21324,#21325,#21326,#21327)) ;
#4379=EDGE_LOOP('',(#21328,#21329,#21330,#21331)) ;
#4380=EDGE_LOOP('',(#21332,#21333,#21334,#21335)) ;
#4381=EDGE_LOOP('',(#21336,#21337,#21338,#21339,#21340,#21341,#21342,#21343,
#21344)) ;
#4382=EDGE_LOOP('',(#21345,#21346,#21347,#21348)) ;
#4383=EDGE_LOOP('',(#21349,#21350,#21351,#21352)) ;
#4384=EDGE_LOOP('',(#21353,#21354,#21355,#21356)) ;
#4385=EDGE_LOOP('',(#21357,#21358,#21359,#21360)) ;
#4386=EDGE_LOOP('',(#21361,#21362,#21363,#21364)) ;
#4387=EDGE_LOOP('',(#21365,#21366,#21367,#21368)) ;
#4388=EDGE_LOOP('',(#21369,#21370,#21371,#21372,#21373)) ;
#4389=EDGE_LOOP('',(#21374,#21375,#21376,#21377,#21378,#21379)) ;
#4390=EDGE_LOOP('',(#21380)) ;
#4391=EDGE_LOOP('',(#21381,#21382,#21383,#21384,#21385,#21386,#21387,#21388,
#21389,#21390,#21391,#21392,#21393,#21394,#21395,#21396,#21397,#21398,#21399,
#21400)) ;
#4392=EDGE_LOOP('',(#21401,#21402,#21403,#21404,#21405,#21406,#21407,#21408)) ;
#4393=EDGE_LOOP('',(#21409,#21410,#21411,#21412,#21413,#21414,#21415,#21416,
#21417,#21418,#21419,#21420,#21421,#21422,#21423,#21424,#21425,#21426,#21427,
#21428,#21429,#21430,#21431)) ;
#4394=EDGE_LOOP('',(#21432,#21433,#21434,#21435)) ;
#4395=EDGE_LOOP('',(#21436,#21437,#21438,#21439)) ;
#4396=EDGE_LOOP('',(#21440,#21441,#21442,#21443)) ;
#4397=EDGE_LOOP('',(#21444,#21445,#21446,#21447)) ;
#4398=EDGE_LOOP('',(#21448,#21449,#21450,#21451)) ;
#4399=EDGE_LOOP('',(#21452,#21453,#21454,#21455)) ;
#4400=EDGE_LOOP('',(#21456,#21457,#21458,#21459)) ;
#4401=EDGE_LOOP('',(#21460,#21461,#21462,#21463)) ;
#4402=EDGE_LOOP('',(#21464,#21465,#21466,#21467)) ;
#4403=EDGE_LOOP('',(#21468,#21469,#21470,#21471)) ;
#4404=EDGE_LOOP('',(#21472,#21473,#21474,#21475)) ;
#4405=EDGE_LOOP('',(#21476,#21477,#21478,#21479)) ;
#4406=EDGE_LOOP('',(#21480,#21481,#21482,#21483)) ;
#4407=EDGE_LOOP('',(#21484,#21485,#21486,#21487)) ;
#4408=EDGE_LOOP('',(#21488,#21489,#21490,#21491,#21492)) ;
#4409=EDGE_LOOP('',(#21493,#21494,#21495,#21496)) ;
#4410=EDGE_LOOP('',(#21497,#21498,#21499,#21500)) ;
#4411=EDGE_LOOP('',(#21501,#21502,#21503,#21504)) ;
#4412=EDGE_LOOP('',(#21505,#21506,#21507,#21508)) ;
#4413=EDGE_LOOP('',(#21509,#21510,#21511,#21512)) ;
#4414=EDGE_LOOP('',(#21513,#21514,#21515,#21516,#21517,#21518)) ;
#4415=EDGE_LOOP('',(#21519)) ;
#4416=EDGE_LOOP('',(#21520,#21521,#21522,#21523,#21524,#21525,#21526,#21527,
#21528,#21529,#21530,#21531,#21532,#21533,#21534,#21535)) ;
#4417=EDGE_LOOP('',(#21536,#21537,#21538,#21539,#21540,#21541,#21542,#21543,
#21544,#21545,#21546,#21547,#21548,#21549)) ;
#6462=LINE('',#48639,#8781) ;
#6463=LINE('',#48651,#8782) ;
#6464=LINE('',#48727,#8783) ;
#6465=LINE('',#48803,#8784) ;
#6466=LINE('',#48879,#8785) ;
#6467=LINE('',#48955,#8786) ;
#6468=LINE('',#49031,#8787) ;
#6469=LINE('',#49058,#8788) ;
#6470=LINE('',#49085,#8789) ;
#6471=LINE('',#49161,#8790) ;
#6472=LINE('',#49237,#8791) ;
#6473=LINE('',#49315,#8792) ;
#6474=LINE('',#49531,#8793) ;
#6475=LINE('',#49537,#8794) ;
#6476=LINE('',#49539,#8795) ;
#6477=LINE('',#49541,#8796) ;
#6478=LINE('',#49543,#8797) ;
#6479=LINE('',#49547,#8798) ;
#6480=LINE('',#49549,#8799) ;
#6481=LINE('',#49551,#8800) ;
#6482=LINE('',#49553,#8801) ;
#6483=LINE('',#49557,#8802) ;
#6484=LINE('',#49559,#8803) ;
#6485=LINE('',#49561,#8804) ;
#6486=LINE('',#49563,#8805) ;
#6487=LINE('',#49567,#8806) ;
#6488=LINE('',#49569,#8807) ;
#6489=LINE('',#49571,#8808) ;
#6490=LINE('',#49572,#8809) ;
#6491=LINE('',#49604,#8810) ;
#6492=LINE('',#49639,#8811) ;
#6493=LINE('',#49723,#8812) ;
#6494=LINE('',#49724,#8813) ;
#6495=LINE('',#49726,#8814) ;
#6496=LINE('',#49729,#8815) ;
#6497=LINE('',#49731,#8816) ;
#6498=LINE('',#49733,#8817) ;
#6499=LINE('',#49736,#8818) ;
#6500=LINE('',#49738,#8819) ;
#6501=LINE('',#49740,#8820) ;
#6502=LINE('',#49746,#8821) ;
#6503=LINE('',#49748,#8822) ;
#6504=LINE('',#49750,#8823) ;
#8781=VECTOR('',#37460,1.00995540144767) ;
#8782=VECTOR('',#37465,1.00995540144767) ;
#8783=VECTOR('',#37470,1.00995540144767) ;
#8784=VECTOR('',#37473,1.00995540144767) ;
#8785=VECTOR('',#37476,1.00995540144767) ;
#8786=VECTOR('',#37479,1.00995540144767) ;
#8787=VECTOR('',#37482,1.4224) ;
#8788=VECTOR('',#37485,1.4224) ;
#8789=VECTOR('',#37494,1.4224) ;
#8790=VECTOR('',#37497,1.4224) ;
#8791=VECTOR('',#37500,1.4224) ;
#8792=VECTOR('',#37503,1.4224) ;
#8793=VECTOR('',#37524,1.4224) ;
#8794=VECTOR('',#37529,1000.) ;
#8795=VECTOR('',#37530,1000.) ;
#8796=VECTOR('',#37531,1000.) ;
#8797=VECTOR('',#37532,1000.) ;
#8798=VECTOR('',#37535,1000.) ;
#8799=VECTOR('',#37536,1000.) ;
#8800=VECTOR('',#37537,1000.) ;
#8801=VECTOR('',#37538,1000.) ;
#8802=VECTOR('',#37541,1000.) ;
#8803=VECTOR('',#37542,1000.) ;
#8804=VECTOR('',#37543,1000.) ;
#8805=VECTOR('',#37544,1000.) ;
#8806=VECTOR('',#37547,1000.) ;
#8807=VECTOR('',#37548,1000.) ;
#8808=VECTOR('',#37549,1000.) ;
#8809=VECTOR('',#37550,1000.) ;
#8810=VECTOR('',#37553,0.92075) ;
#8811=VECTOR('',#37558,0.968718914342085) ;
#8812=VECTOR('',#37589,1000.) ;
#8813=VECTOR('',#37590,1000.) ;
#8814=VECTOR('',#37593,1000.) ;
#8815=VECTOR('',#37598,1000.) ;
#8816=VECTOR('',#37601,1000.) ;
#8817=VECTOR('',#37604,1000.) ;
#8818=VECTOR('',#37609,1000.) ;
#8819=VECTOR('',#37612,1000.) ;
#8820=VECTOR('',#37615,1000.) ;
#8821=VECTOR('',#37626,1000.) ;
#8822=VECTOR('',#37629,1000.) ;
#8823=VECTOR('',#37632,1000.) ;
#11051=CIRCLE('',#33126,1.00995540144767) ;
#11052=CIRCLE('',#33128,1.00995540144767) ;
#11053=CIRCLE('',#33134,1.4224) ;
#11054=CIRCLE('',#33135,1.42240000000001) ;
#11055=CIRCLE('',#33136,1.42240000000001) ;
#11056=CIRCLE('',#33137,1.4224) ;
#11057=CIRCLE('',#33143,1.4224) ;
#11058=CIRCLE('',#33145,1.00995540144768) ;
#11059=CIRCLE('',#33147,2.55525626680218) ;
#11060=CIRCLE('',#33148,0.0625) ;
#11061=CIRCLE('',#33149,2.60242561556611) ;
#11062=CIRCLE('',#33150,2.60242561556611) ;
#11063=CIRCLE('',#33153,1.7907) ;
#11064=CIRCLE('',#33154,1.7907) ;
#11065=CIRCLE('',#33155,1.7907) ;
#11066=CIRCLE('',#33156,1.7907) ;
#11067=CIRCLE('',#33158,0.92075) ;
#11068=CIRCLE('',#33160,1.7907) ;
#11069=CIRCLE('',#33161,1.7907) ;
#11070=CIRCLE('',#33162,1.7907) ;
#11071=CIRCLE('',#33163,1.7907) ;
#11072=CIRCLE('',#33164,1.7907) ;
#12970=VERTEX_POINT('',#48637) ;
#12971=VERTEX_POINT('',#48638) ;
#12972=VERTEX_POINT('',#48640) ;
#12973=VERTEX_POINT('',#48649) ;
#12974=VERTEX_POINT('',#48650) ;
#12975=VERTEX_POINT('',#48688) ;
#12976=VERTEX_POINT('',#48725) ;
#12977=VERTEX_POINT('',#48726) ;
#12978=VERTEX_POINT('',#48801) ;
#12979=VERTEX_POINT('',#48802) ;
#12980=VERTEX_POINT('',#48877) ;
#12981=VERTEX_POINT('',#48878) ;
#12982=VERTEX_POINT('',#48953) ;
#12983=VERTEX_POINT('',#48954) ;
#12984=VERTEX_POINT('',#49029) ;
#12985=VERTEX_POINT('',#49030) ;
#12986=VERTEX_POINT('',#49032) ;
#12987=VERTEX_POINT('',#49055) ;
#12988=VERTEX_POINT('',#49057) ;
#12989=VERTEX_POINT('',#49059) ;
#12990=VERTEX_POINT('',#49062) ;
#12991=VERTEX_POINT('',#49083) ;
#12992=VERTEX_POINT('',#49084) ;
#12993=VERTEX_POINT('',#49159) ;
#12994=VERTEX_POINT('',#49160) ;
#12995=VERTEX_POINT('',#49235) ;
#12996=VERTEX_POINT('',#49236) ;
#12997=VERTEX_POINT('',#49313) ;
#12998=VERTEX_POINT('',#49314) ;
#12999=VERTEX_POINT('',#49391) ;
#13000=VERTEX_POINT('',#49422) ;
#13001=VERTEX_POINT('',#49451) ;
#13002=VERTEX_POINT('',#49488) ;
#13003=VERTEX_POINT('',#49523) ;
#13004=VERTEX_POINT('',#49525) ;
#13005=VERTEX_POINT('',#49527) ;
#13006=VERTEX_POINT('',#49533) ;
#13007=VERTEX_POINT('',#49534) ;
#13008=VERTEX_POINT('',#49536) ;
#13009=VERTEX_POINT('',#49538) ;
#13010=VERTEX_POINT('',#49540) ;
#13011=VERTEX_POINT('',#49542) ;
#13012=VERTEX_POINT('',#49544) ;
#13013=VERTEX_POINT('',#49546) ;
#13014=VERTEX_POINT('',#49548) ;
#13015=VERTEX_POINT('',#49550) ;
#13016=VERTEX_POINT('',#49552) ;
#13017=VERTEX_POINT('',#49554) ;
#13018=VERTEX_POINT('',#49556) ;
#13019=VERTEX_POINT('',#49558) ;
#13020=VERTEX_POINT('',#49560) ;
#13021=VERTEX_POINT('',#49562) ;
#13022=VERTEX_POINT('',#49564) ;
#13023=VERTEX_POINT('',#49566) ;
#13024=VERTEX_POINT('',#49568) ;
#13025=VERTEX_POINT('',#49570) ;
#13026=VERTEX_POINT('',#49574) ;
#13027=VERTEX_POINT('',#49603) ;
#13028=VERTEX_POINT('',#49637) ;
#13029=VERTEX_POINT('',#49638) ;
#13030=VERTEX_POINT('',#49640) ;
#13031=VERTEX_POINT('',#49642) ;
#13032=VERTEX_POINT('',#49646) ;
#13033=VERTEX_POINT('',#49650) ;
#13034=VERTEX_POINT('',#49654) ;
#13035=VERTEX_POINT('',#49658) ;
#13036=VERTEX_POINT('',#49660) ;
#13037=VERTEX_POINT('',#49664) ;
#13038=VERTEX_POINT('',#49668) ;
#13039=VERTEX_POINT('',#49672) ;
#13040=VERTEX_POINT('',#49676) ;
#13041=VERTEX_POINT('',#49678) ;
#13042=VERTEX_POINT('',#49682) ;
#13043=VERTEX_POINT('',#49686) ;
#13044=VERTEX_POINT('',#49690) ;
#13045=VERTEX_POINT('',#49694) ;
#13046=VERTEX_POINT('',#49696) ;
#13047=VERTEX_POINT('',#49700) ;
#13048=VERTEX_POINT('',#49704) ;
#13049=VERTEX_POINT('',#49708) ;
#16062=EDGE_CURVE('',#12970,#12971,#6462,.T.) ;
#16063=EDGE_CURVE('',#12970,#12972,#1226,.T.) ;
#16064=EDGE_CURVE('',#12972,#12971,#11051,.T.) ;
#16065=EDGE_CURVE('',#12973,#12974,#6463,.T.) ;
#16066=EDGE_CURVE('',#12973,#12970,#1227,.T.) ;
#16067=EDGE_CURVE('',#12971,#12975,#11052,.T.) ;
#16068=EDGE_CURVE('',#12974,#12975,#1228,.F.) ;
#16069=EDGE_CURVE('',#12976,#12977,#6464,.T.) ;
#16070=EDGE_CURVE('',#12976,#12973,#1229,.T.) ;
#16071=EDGE_CURVE('',#12977,#12974,#1230,.F.) ;
#16072=EDGE_CURVE('',#12978,#12979,#6465,.T.) ;
#16073=EDGE_CURVE('',#12978,#12976,#1231,.T.) ;
#16074=EDGE_CURVE('',#12979,#12977,#1232,.F.) ;
#16075=EDGE_CURVE('',#12980,#12981,#6466,.T.) ;
#16076=EDGE_CURVE('',#12980,#12978,#1233,.T.) ;
#16077=EDGE_CURVE('',#12981,#12979,#1234,.F.) ;
#16078=EDGE_CURVE('',#12982,#12983,#6467,.T.) ;
#16079=EDGE_CURVE('',#12982,#12980,#1235,.T.) ;
#16080=EDGE_CURVE('',#12983,#12981,#1236,.F.) ;
#16081=EDGE_CURVE('',#12984,#12985,#6468,.T.) ;
#16082=EDGE_CURVE('',#12986,#12984,#1237,.F.) ;
#16083=EDGE_CURVE('',#12986,#12987,#11053,.T.) ;
#16084=EDGE_CURVE('',#12987,#12988,#6469,.T.) ;
#16085=EDGE_CURVE('',#12988,#12989,#11054,.T.) ;
#16086=EDGE_CURVE('',#12989,#12988,#11055,.T.) ;
#16087=EDGE_CURVE('',#12987,#12990,#11056,.T.) ;
#16088=EDGE_CURVE('',#12985,#12990,#1238,.F.) ;
#16089=EDGE_CURVE('',#12991,#12992,#6470,.T.) ;
#16090=EDGE_CURVE('',#12984,#12991,#1239,.F.) ;
#16091=EDGE_CURVE('',#12992,#12985,#1240,.F.) ;
#16092=EDGE_CURVE('',#12993,#12994,#6471,.T.) ;
#16093=EDGE_CURVE('',#12991,#12993,#1241,.F.) ;
#16094=EDGE_CURVE('',#12994,#12992,#1242,.F.) ;
#16095=EDGE_CURVE('',#12995,#12996,#6472,.T.) ;
#16096=EDGE_CURVE('',#12993,#12995,#1243,.F.) ;
#16097=EDGE_CURVE('',#12996,#12994,#1244,.F.) ;
#16098=EDGE_CURVE('',#12997,#12998,#6473,.T.) ;
#16099=EDGE_CURVE('',#12995,#12997,#1245,.F.) ;
#16100=EDGE_CURVE('',#12998,#12996,#1246,.F.) ;
#16101=EDGE_CURVE('',#12999,#12998,#1247,.F.) ;
#16102=EDGE_CURVE('',#13000,#12999,#11057,.T.) ;
#16103=EDGE_CURVE('',#12997,#13000,#1248,.F.) ;
#16104=EDGE_CURVE('',#13001,#12983,#1249,.F.) ;
#16105=EDGE_CURVE('',#13002,#13001,#11058,.T.) ;
#16106=EDGE_CURVE('',#13002,#12982,#1250,.T.) ;
#16107=EDGE_CURVE('',#13003,#13003,#11059,.T.) ;
#16108=EDGE_CURVE('',#13003,#13004,#11060,.T.) ;
#16109=EDGE_CURVE('',#13004,#13005,#11061,.T.) ;
#16110=EDGE_CURVE('',#13005,#13004,#11062,.T.) ;
#16111=EDGE_CURVE('',#13005,#12989,#6474,.T.) ;
#16112=EDGE_CURVE('',#13006,#13007,#11063,.T.) ;
#16113=EDGE_CURVE('',#13006,#13008,#6475,.T.) ;
#16114=EDGE_CURVE('',#13008,#13009,#6476,.T.) ;
#16115=EDGE_CURVE('',#13009,#13010,#6477,.T.) ;
#16116=EDGE_CURVE('',#13011,#13010,#6478,.T.) ;
#16117=EDGE_CURVE('',#13012,#13011,#11064,.T.) ;
#16118=EDGE_CURVE('',#13012,#13013,#6479,.T.) ;
#16119=EDGE_CURVE('',#13013,#13014,#6480,.T.) ;
#16120=EDGE_CURVE('',#13014,#13015,#6481,.T.) ;
#16121=EDGE_CURVE('',#13016,#13015,#6482,.T.) ;
#16122=EDGE_CURVE('',#13017,#13016,#11065,.T.) ;
#16123=EDGE_CURVE('',#13017,#13018,#6483,.T.) ;
#16124=EDGE_CURVE('',#13018,#13019,#6484,.T.) ;
#16125=EDGE_CURVE('',#13019,#13020,#6485,.T.) ;
#16126=EDGE_CURVE('',#13021,#13020,#6486,.T.) ;
#16127=EDGE_CURVE('',#13021,#13022,#11066,.T.) ;
#16128=EDGE_CURVE('',#13022,#13023,#6487,.T.) ;
#16129=EDGE_CURVE('',#13023,#13024,#6488,.T.) ;
#16130=EDGE_CURVE('',#13024,#13025,#6489,.T.) ;
#16131=EDGE_CURVE('',#13007,#13025,#6490,.T.) ;
#16132=EDGE_CURVE('',#12999,#13026,#1251,.F.) ;
#16133=EDGE_CURVE('',#13026,#13027,#6491,.T.) ;
#16134=EDGE_CURVE('',#13027,#13027,#11067,.T.) ;
#16135=EDGE_CURVE('',#13026,#13002,#1252,.F.) ;
#16136=EDGE_CURVE('',#13001,#13000,#1253,.T.) ;
#16137=EDGE_CURVE('',#13028,#13029,#6492,.T.) ;
#16138=EDGE_CURVE('',#13029,#13030,#11068,.T.) ;
#16139=EDGE_CURVE('',#13031,#13030,#788,.T.) ;
#16140=EDGE_CURVE('',#13031,#13032,#789,.T.) ;
#16141=EDGE_CURVE('',#13032,#13033,#790,.T.) ;
#16142=EDGE_CURVE('',#13033,#13034,#791,.T.) ;
#16143=EDGE_CURVE('',#13035,#13034,#11069,.T.) ;
#16144=EDGE_CURVE('',#13036,#13035,#792,.T.) ;
#16145=EDGE_CURVE('',#13036,#13037,#793,.T.) ;
#16146=EDGE_CURVE('',#13037,#13038,#794,.T.) ;
#16147=EDGE_CURVE('',#13038,#13039,#795,.T.) ;
#16148=EDGE_CURVE('',#13040,#13039,#11070,.T.) ;
#16149=EDGE_CURVE('',#13041,#13040,#796,.T.) ;
#16150=EDGE_CURVE('',#13041,#13042,#797,.T.) ;
#16151=EDGE_CURVE('',#13042,#13043,#798,.T.) ;
#16152=EDGE_CURVE('',#13043,#13044,#799,.T.) ;
#16153=EDGE_CURVE('',#13045,#13044,#11071,.T.) ;
#16154=EDGE_CURVE('',#13046,#13045,#800,.T.) ;
#16155=EDGE_CURVE('',#13046,#13047,#801,.T.) ;
#16156=EDGE_CURVE('',#13047,#13048,#802,.T.) ;
#16157=EDGE_CURVE('',#13048,#13049,#803,.T.) ;
#16158=EDGE_CURVE('',#13049,#13029,#11072,.T.) ;
#16159=EDGE_CURVE('',#13044,#13006,#122,.T.) ;
#16160=EDGE_CURVE('',#13045,#13007,#123,.T.) ;
#16161=EDGE_CURVE('',#13034,#13017,#124,.T.) ;
#16162=EDGE_CURVE('',#13035,#13016,#125,.T.) ;
#16163=EDGE_CURVE('',#13039,#13012,#126,.T.) ;
#16164=EDGE_CURVE('',#13040,#13011,#127,.T.) ;
#16165=EDGE_CURVE('',#13042,#13009,#6493,.T.) ;
#16166=EDGE_CURVE('',#13043,#13008,#6494,.T.) ;
#16167=EDGE_CURVE('',#13041,#13010,#6495,.T.) ;
#16168=EDGE_CURVE('',#13038,#13013,#6496,.T.) ;
#16169=EDGE_CURVE('',#13037,#13014,#6497,.T.) ;
#16170=EDGE_CURVE('',#13036,#13015,#6498,.T.) ;
#16171=EDGE_CURVE('',#13033,#13018,#6499,.T.) ;
#16172=EDGE_CURVE('',#13032,#13019,#6500,.T.) ;
#16173=EDGE_CURVE('',#13031,#13020,#6501,.T.) ;
#16174=EDGE_CURVE('',#13030,#13021,#128,.T.) ;
#16175=EDGE_CURVE('',#13049,#13022,#129,.T.) ;
#16176=EDGE_CURVE('',#13048,#13023,#6502,.T.) ;
#16177=EDGE_CURVE('',#13047,#13024,#6503,.T.) ;
#16178=EDGE_CURVE('',#13046,#13025,#6504,.T.) ;
#16179=EDGE_CURVE('',#12990,#12972,#1254,.T.) ;
#16180=EDGE_CURVE('',#12975,#12986,#1255,.T.) ;
#21312=ORIENTED_EDGE('',*,*,#16062,.F.) ;
#21313=ORIENTED_EDGE('',*,*,#16063,.T.) ;
#21314=ORIENTED_EDGE('',*,*,#16064,.T.) ;
#21315=ORIENTED_EDGE('',*,*,#16065,.F.) ;
#21316=ORIENTED_EDGE('',*,*,#16066,.T.) ;
#21317=ORIENTED_EDGE('',*,*,#16062,.T.) ;
#21318=ORIENTED_EDGE('',*,*,#16067,.T.) ;
#21319=ORIENTED_EDGE('',*,*,#16068,.F.) ;
#21320=ORIENTED_EDGE('',*,*,#16069,.F.) ;
#21321=ORIENTED_EDGE('',*,*,#16070,.T.) ;
#21322=ORIENTED_EDGE('',*,*,#16065,.T.) ;
#21323=ORIENTED_EDGE('',*,*,#16071,.F.) ;
#21324=ORIENTED_EDGE('',*,*,#16072,.F.) ;
#21325=ORIENTED_EDGE('',*,*,#16073,.T.) ;
#21326=ORIENTED_EDGE('',*,*,#16069,.T.) ;
#21327=ORIENTED_EDGE('',*,*,#16074,.F.) ;
#21328=ORIENTED_EDGE('',*,*,#16075,.F.) ;
#21329=ORIENTED_EDGE('',*,*,#16076,.T.) ;
#21330=ORIENTED_EDGE('',*,*,#16072,.T.) ;
#21331=ORIENTED_EDGE('',*,*,#16077,.F.) ;
#21332=ORIENTED_EDGE('',*,*,#16078,.F.) ;
#21333=ORIENTED_EDGE('',*,*,#16079,.T.) ;
#21334=ORIENTED_EDGE('',*,*,#16075,.T.) ;
#21335=ORIENTED_EDGE('',*,*,#16080,.F.) ;
#21336=ORIENTED_EDGE('',*,*,#16081,.F.) ;
#21337=ORIENTED_EDGE('',*,*,#16082,.F.) ;
#21338=ORIENTED_EDGE('',*,*,#16083,.T.) ;
#21339=ORIENTED_EDGE('',*,*,#16084,.T.) ;
#21340=ORIENTED_EDGE('',*,*,#16085,.T.) ;
#21341=ORIENTED_EDGE('',*,*,#16086,.T.) ;
#21342=ORIENTED_EDGE('',*,*,#16084,.F.) ;
#21343=ORIENTED_EDGE('',*,*,#16087,.T.) ;
#21344=ORIENTED_EDGE('',*,*,#16088,.F.) ;
#21345=ORIENTED_EDGE('',*,*,#16089,.F.) ;
#21346=ORIENTED_EDGE('',*,*,#16090,.F.) ;
#21347=ORIENTED_EDGE('',*,*,#16081,.T.) ;
#21348=ORIENTED_EDGE('',*,*,#16091,.F.) ;
#21349=ORIENTED_EDGE('',*,*,#16092,.F.) ;
#21350=ORIENTED_EDGE('',*,*,#16093,.F.) ;
#21351=ORIENTED_EDGE('',*,*,#16089,.T.) ;
#21352=ORIENTED_EDGE('',*,*,#16094,.F.) ;
#21353=ORIENTED_EDGE('',*,*,#16095,.F.) ;
#21354=ORIENTED_EDGE('',*,*,#16096,.F.) ;
#21355=ORIENTED_EDGE('',*,*,#16092,.T.) ;
#21356=ORIENTED_EDGE('',*,*,#16097,.F.) ;
#21357=ORIENTED_EDGE('',*,*,#16098,.F.) ;
#21358=ORIENTED_EDGE('',*,*,#16099,.F.) ;
#21359=ORIENTED_EDGE('',*,*,#16095,.T.) ;
#21360=ORIENTED_EDGE('',*,*,#16100,.F.) ;
#21361=ORIENTED_EDGE('',*,*,#16098,.T.) ;
#21362=ORIENTED_EDGE('',*,*,#16101,.F.) ;
#21363=ORIENTED_EDGE('',*,*,#16102,.F.) ;
#21364=ORIENTED_EDGE('',*,*,#16103,.F.) ;
#21365=ORIENTED_EDGE('',*,*,#16078,.T.) ;
#21366=ORIENTED_EDGE('',*,*,#16104,.F.) ;
#21367=ORIENTED_EDGE('',*,*,#16105,.F.) ;
#21368=ORIENTED_EDGE('',*,*,#16106,.T.) ;
#21369=ORIENTED_EDGE('',*,*,#16107,.T.) ;
#21370=ORIENTED_EDGE('',*,*,#16108,.T.) ;
#21371=ORIENTED_EDGE('',*,*,#16109,.T.) ;
#21372=ORIENTED_EDGE('',*,*,#16110,.T.) ;
#21373=ORIENTED_EDGE('',*,*,#16108,.F.) ;
#21374=ORIENTED_EDGE('',*,*,#16110,.F.) ;
#21375=ORIENTED_EDGE('',*,*,#16111,.T.) ;
#21376=ORIENTED_EDGE('',*,*,#16085,.F.) ;
#21377=ORIENTED_EDGE('',*,*,#16086,.F.) ;
#21378=ORIENTED_EDGE('',*,*,#16111,.F.) ;
#21379=ORIENTED_EDGE('',*,*,#16109,.F.) ;
#21380=ORIENTED_EDGE('',*,*,#16107,.F.) ;
#21381=ORIENTED_EDGE('',*,*,#16112,.F.) ;
#21382=ORIENTED_EDGE('',*,*,#16113,.T.) ;
#21383=ORIENTED_EDGE('',*,*,#16114,.T.) ;
#21384=ORIENTED_EDGE('',*,*,#16115,.T.) ;
#21385=ORIENTED_EDGE('',*,*,#16116,.F.) ;
#21386=ORIENTED_EDGE('',*,*,#16117,.F.) ;
#21387=ORIENTED_EDGE('',*,*,#16118,.T.) ;
#21388=ORIENTED_EDGE('',*,*,#16119,.T.) ;
#21389=ORIENTED_EDGE('',*,*,#16120,.T.) ;
#21390=ORIENTED_EDGE('',*,*,#16121,.F.) ;
#21391=ORIENTED_EDGE('',*,*,#16122,.F.) ;
#21392=ORIENTED_EDGE('',*,*,#16123,.T.) ;
#21393=ORIENTED_EDGE('',*,*,#16124,.T.) ;
#21394=ORIENTED_EDGE('',*,*,#16125,.T.) ;
#21395=ORIENTED_EDGE('',*,*,#16126,.F.) ;
#21396=ORIENTED_EDGE('',*,*,#16127,.T.) ;
#21397=ORIENTED_EDGE('',*,*,#16128,.T.) ;
#21398=ORIENTED_EDGE('',*,*,#16129,.T.) ;
#21399=ORIENTED_EDGE('',*,*,#16130,.T.) ;
#21400=ORIENTED_EDGE('',*,*,#16131,.F.) ;
#21401=ORIENTED_EDGE('',*,*,#16132,.T.) ;
#21402=ORIENTED_EDGE('',*,*,#16133,.T.) ;
#21403=ORIENTED_EDGE('',*,*,#16134,.F.) ;
#21404=ORIENTED_EDGE('',*,*,#16133,.F.) ;
#21405=ORIENTED_EDGE('',*,*,#16135,.T.) ;
#21406=ORIENTED_EDGE('',*,*,#16105,.T.) ;
#21407=ORIENTED_EDGE('',*,*,#16136,.T.) ;
#21408=ORIENTED_EDGE('',*,*,#16102,.T.) ;
#21409=ORIENTED_EDGE('',*,*,#16137,.T.) ;
#21410=ORIENTED_EDGE('',*,*,#16138,.T.) ;
#21411=ORIENTED_EDGE('',*,*,#16139,.F.) ;
#21412=ORIENTED_EDGE('',*,*,#16140,.T.) ;
#21413=ORIENTED_EDGE('',*,*,#16141,.T.) ;
#21414=ORIENTED_EDGE('',*,*,#16142,.T.) ;
#21415=ORIENTED_EDGE('',*,*,#16143,.F.) ;
#21416=ORIENTED_EDGE('',*,*,#16144,.F.) ;
#21417=ORIENTED_EDGE('',*,*,#16145,.T.) ;
#21418=ORIENTED_EDGE('',*,*,#16146,.T.) ;
#21419=ORIENTED_EDGE('',*,*,#16147,.T.) ;
#21420=ORIENTED_EDGE('',*,*,#16148,.F.) ;
#21421=ORIENTED_EDGE('',*,*,#16149,.F.) ;
#21422=ORIENTED_EDGE('',*,*,#16150,.T.) ;
#21423=ORIENTED_EDGE('',*,*,#16151,.T.) ;
#21424=ORIENTED_EDGE('',*,*,#16152,.T.) ;
#21425=ORIENTED_EDGE('',*,*,#16153,.F.) ;
#21426=ORIENTED_EDGE('',*,*,#16154,.F.) ;
#21427=ORIENTED_EDGE('',*,*,#16155,.T.) ;
#21428=ORIENTED_EDGE('',*,*,#16156,.T.) ;
#21429=ORIENTED_EDGE('',*,*,#16157,.T.) ;
#21430=ORIENTED_EDGE('',*,*,#16158,.T.) ;
#21431=ORIENTED_EDGE('',*,*,#16137,.F.) ;
#21432=ORIENTED_EDGE('',*,*,#16153,.T.) ;
#21433=ORIENTED_EDGE('',*,*,#16159,.T.) ;
#21434=ORIENTED_EDGE('',*,*,#16112,.T.) ;
#21435=ORIENTED_EDGE('',*,*,#16160,.F.) ;
#21436=ORIENTED_EDGE('',*,*,#16143,.T.) ;
#21437=ORIENTED_EDGE('',*,*,#16161,.T.) ;
#21438=ORIENTED_EDGE('',*,*,#16122,.T.) ;
#21439=ORIENTED_EDGE('',*,*,#16162,.F.) ;
#21440=ORIENTED_EDGE('',*,*,#16148,.T.) ;
#21441=ORIENTED_EDGE('',*,*,#16163,.T.) ;
#21442=ORIENTED_EDGE('',*,*,#16117,.T.) ;
#21443=ORIENTED_EDGE('',*,*,#16164,.F.) ;
#21444=ORIENTED_EDGE('',*,*,#16165,.T.) ;
#21445=ORIENTED_EDGE('',*,*,#16114,.F.) ;
#21446=ORIENTED_EDGE('',*,*,#16166,.F.) ;
#21447=ORIENTED_EDGE('',*,*,#16151,.F.) ;
#21448=ORIENTED_EDGE('',*,*,#16167,.T.) ;
#21449=ORIENTED_EDGE('',*,*,#16115,.F.) ;
#21450=ORIENTED_EDGE('',*,*,#16165,.F.) ;
#21451=ORIENTED_EDGE('',*,*,#16150,.F.) ;
#21452=ORIENTED_EDGE('',*,*,#16149,.T.) ;
#21453=ORIENTED_EDGE('',*,*,#16164,.T.) ;
#21454=ORIENTED_EDGE('',*,*,#16116,.T.) ;
#21455=ORIENTED_EDGE('',*,*,#16167,.F.) ;
#21456=ORIENTED_EDGE('',*,*,#16168,.T.) ;
#21457=ORIENTED_EDGE('',*,*,#16118,.F.) ;
#21458=ORIENTED_EDGE('',*,*,#16163,.F.) ;
#21459=ORIENTED_EDGE('',*,*,#16147,.F.) ;
#21460=ORIENTED_EDGE('',*,*,#16169,.T.) ;
#21461=ORIENTED_EDGE('',*,*,#16119,.F.) ;
#21462=ORIENTED_EDGE('',*,*,#16168,.F.) ;
#21463=ORIENTED_EDGE('',*,*,#16146,.F.) ;
#21464=ORIENTED_EDGE('',*,*,#16170,.T.) ;
#21465=ORIENTED_EDGE('',*,*,#16120,.F.) ;
#21466=ORIENTED_EDGE('',*,*,#16169,.F.) ;
#21467=ORIENTED_EDGE('',*,*,#16145,.F.) ;
#21468=ORIENTED_EDGE('',*,*,#16144,.T.) ;
#21469=ORIENTED_EDGE('',*,*,#16162,.T.) ;
#21470=ORIENTED_EDGE('',*,*,#16121,.T.) ;
#21471=ORIENTED_EDGE('',*,*,#16170,.F.) ;
#21472=ORIENTED_EDGE('',*,*,#16171,.T.) ;
#21473=ORIENTED_EDGE('',*,*,#16123,.F.) ;
#21474=ORIENTED_EDGE('',*,*,#16161,.F.) ;
#21475=ORIENTED_EDGE('',*,*,#16142,.F.) ;
#21476=ORIENTED_EDGE('',*,*,#16172,.T.) ;
#21477=ORIENTED_EDGE('',*,*,#16124,.F.) ;
#21478=ORIENTED_EDGE('',*,*,#16171,.F.) ;
#21479=ORIENTED_EDGE('',*,*,#16141,.F.) ;
#21480=ORIENTED_EDGE('',*,*,#16173,.T.) ;
#21481=ORIENTED_EDGE('',*,*,#16125,.F.) ;
#21482=ORIENTED_EDGE('',*,*,#16172,.F.) ;
#21483=ORIENTED_EDGE('',*,*,#16140,.F.) ;
#21484=ORIENTED_EDGE('',*,*,#16139,.T.) ;
#21485=ORIENTED_EDGE('',*,*,#16174,.T.) ;
#21486=ORIENTED_EDGE('',*,*,#16126,.T.) ;
#21487=ORIENTED_EDGE('',*,*,#16173,.F.) ;
#21488=ORIENTED_EDGE('',*,*,#16175,.T.) ;
#21489=ORIENTED_EDGE('',*,*,#16127,.F.) ;
#21490=ORIENTED_EDGE('',*,*,#16174,.F.) ;
#21491=ORIENTED_EDGE('',*,*,#16138,.F.) ;
#21492=ORIENTED_EDGE('',*,*,#16158,.F.) ;
#21493=ORIENTED_EDGE('',*,*,#16176,.T.) ;
#21494=ORIENTED_EDGE('',*,*,#16128,.F.) ;
#21495=ORIENTED_EDGE('',*,*,#16175,.F.) ;
#21496=ORIENTED_EDGE('',*,*,#16157,.F.) ;
#21497=ORIENTED_EDGE('',*,*,#16177,.T.) ;
#21498=ORIENTED_EDGE('',*,*,#16129,.F.) ;
#21499=ORIENTED_EDGE('',*,*,#16176,.F.) ;
#21500=ORIENTED_EDGE('',*,*,#16156,.F.) ;
#21501=ORIENTED_EDGE('',*,*,#16178,.T.) ;
#21502=ORIENTED_EDGE('',*,*,#16130,.F.) ;
#21503=ORIENTED_EDGE('',*,*,#16177,.F.) ;
#21504=ORIENTED_EDGE('',*,*,#16155,.F.) ;
#21505=ORIENTED_EDGE('',*,*,#16154,.T.) ;
#21506=ORIENTED_EDGE('',*,*,#16160,.T.) ;
#21507=ORIENTED_EDGE('',*,*,#16131,.T.) ;
#21508=ORIENTED_EDGE('',*,*,#16178,.F.) ;
#21509=ORIENTED_EDGE('',*,*,#16166,.T.) ;
#21510=ORIENTED_EDGE('',*,*,#16113,.F.) ;
#21511=ORIENTED_EDGE('',*,*,#16159,.F.) ;
#21512=ORIENTED_EDGE('',*,*,#16152,.F.) ;
#21513=ORIENTED_EDGE('',*,*,#16179,.F.) ;
#21514=ORIENTED_EDGE('',*,*,#16087,.F.) ;
#21515=ORIENTED_EDGE('',*,*,#16083,.F.) ;
#21516=ORIENTED_EDGE('',*,*,#16180,.F.) ;
#21517=ORIENTED_EDGE('',*,*,#16067,.F.) ;
#21518=ORIENTED_EDGE('',*,*,#16064,.F.) ;
#21519=ORIENTED_EDGE('',*,*,#16134,.T.) ;
#21520=ORIENTED_EDGE('',*,*,#16179,.T.) ;
#21521=ORIENTED_EDGE('',*,*,#16063,.F.) ;
#21522=ORIENTED_EDGE('',*,*,#16066,.F.) ;
#21523=ORIENTED_EDGE('',*,*,#16070,.F.) ;
#21524=ORIENTED_EDGE('',*,*,#16073,.F.) ;
#21525=ORIENTED_EDGE('',*,*,#16076,.F.) ;
#21526=ORIENTED_EDGE('',*,*,#16079,.F.) ;
#21527=ORIENTED_EDGE('',*,*,#16106,.F.) ;
#21528=ORIENTED_EDGE('',*,*,#16135,.F.) ;
#21529=ORIENTED_EDGE('',*,*,#16132,.F.) ;
#21530=ORIENTED_EDGE('',*,*,#16101,.T.) ;
#21531=ORIENTED_EDGE('',*,*,#16100,.T.) ;
#21532=ORIENTED_EDGE('',*,*,#16097,.T.) ;
#21533=ORIENTED_EDGE('',*,*,#16094,.T.) ;
#21534=ORIENTED_EDGE('',*,*,#16091,.T.) ;
#21535=ORIENTED_EDGE('',*,*,#16088,.T.) ;
#21536=ORIENTED_EDGE('',*,*,#16180,.T.) ;
#21537=ORIENTED_EDGE('',*,*,#16082,.T.) ;
#21538=ORIENTED_EDGE('',*,*,#16090,.T.) ;
#21539=ORIENTED_EDGE('',*,*,#16093,.T.) ;
#21540=ORIENTED_EDGE('',*,*,#16096,.T.) ;
#21541=ORIENTED_EDGE('',*,*,#16099,.T.) ;
#21542=ORIENTED_EDGE('',*,*,#16103,.T.) ;
#21543=ORIENTED_EDGE('',*,*,#16136,.F.) ;
#21544=ORIENTED_EDGE('',*,*,#16104,.T.) ;
#21545=ORIENTED_EDGE('',*,*,#16080,.T.) ;
#21546=ORIENTED_EDGE('',*,*,#16077,.T.) ;
#21547=ORIENTED_EDGE('',*,*,#16074,.T.) ;
#21548=ORIENTED_EDGE('',*,*,#16071,.T.) ;
#21549=ORIENTED_EDGE('',*,*,#16068,.T.) ;
#30039=CYLINDRICAL_SURFACE('',#33125,1.00995540144767) ;
#30040=CYLINDRICAL_SURFACE('',#33127,1.00995540144767) ;
#30041=CYLINDRICAL_SURFACE('',#33129,1.00995540144767) ;
#30042=CYLINDRICAL_SURFACE('',#33130,1.00995540144767) ;
#30043=CYLINDRICAL_SURFACE('',#33131,1.00995540144767) ;
#30044=CYLINDRICAL_SURFACE('',#33132,1.00995540144767) ;
#30045=CYLINDRICAL_SURFACE('',#33133,1.4224) ;
#30046=CYLINDRICAL_SURFACE('',#33138,1.4224) ;
#30047=CYLINDRICAL_SURFACE('',#33139,1.4224) ;
#30048=CYLINDRICAL_SURFACE('',#33140,1.4224) ;
#30049=CYLINDRICAL_SURFACE('',#33141,1.4224) ;
#30050=CYLINDRICAL_SURFACE('',#33142,1.4224) ;
#30051=CYLINDRICAL_SURFACE('',#33144,1.00995540144767) ;
#30052=CYLINDRICAL_SURFACE('',#33165,1.7907) ;
#30053=CYLINDRICAL_SURFACE('',#33168,1.7907) ;
#30054=CYLINDRICAL_SURFACE('',#33171,1.7907) ;
#30055=CYLINDRICAL_SURFACE('',#33186,1.7907) ;
#30916=ADVANCED_FACE('',(#2437),#30039,.T.) ;
#30917=ADVANCED_FACE('',(#2438),#30040,.T.) ;
#30918=ADVANCED_FACE('',(#2439),#30041,.T.) ;
#30919=ADVANCED_FACE('',(#2440),#30042,.T.) ;
#30920=ADVANCED_FACE('',(#2441),#30043,.T.) ;
#30921=ADVANCED_FACE('',(#2442),#30044,.T.) ;
#30922=ADVANCED_FACE('',(#2443),#30045,.T.) ;
#30923=ADVANCED_FACE('',(#2444),#30046,.T.) ;
#30924=ADVANCED_FACE('',(#2445),#30047,.T.) ;
#30925=ADVANCED_FACE('',(#2446),#30048,.T.) ;
#30926=ADVANCED_FACE('',(#2447),#30049,.T.) ;
#30927=ADVANCED_FACE('',(#2448),#30050,.T.) ;
#30928=ADVANCED_FACE('',(#2449),#30051,.T.) ;
#30929=ADVANCED_FACE('',(#2450),#226,.T.) ;
#30930=ADVANCED_FACE('',(#2451),#880,.T.) ;
#30931=ADVANCED_FACE('',(#2452,#1050),#1760,.F.) ;
#30932=ADVANCED_FACE('',(#2453),#881,.T.) ;
#30933=ADVANCED_FACE('',(#2454),#882,.F.) ;
#30934=ADVANCED_FACE('',(#2455),#30052,.F.) ;
#30935=ADVANCED_FACE('',(#2456),#30053,.F.) ;
#30936=ADVANCED_FACE('',(#2457),#30054,.F.) ;
#30937=ADVANCED_FACE('',(#2458),#1761,.T.) ;
#30938=ADVANCED_FACE('',(#2459),#1762,.T.) ;
#30939=ADVANCED_FACE('',(#2460),#1763,.T.) ;
#30940=ADVANCED_FACE('',(#2461),#1764,.T.) ;
#30941=ADVANCED_FACE('',(#2462),#1765,.T.) ;
#30942=ADVANCED_FACE('',(#2463),#1766,.T.) ;
#30943=ADVANCED_FACE('',(#2464),#1767,.T.) ;
#30944=ADVANCED_FACE('',(#2465),#1768,.T.) ;
#30945=ADVANCED_FACE('',(#2466),#1769,.T.) ;
#30946=ADVANCED_FACE('',(#2467),#1770,.T.) ;
#30947=ADVANCED_FACE('',(#2468),#1771,.T.) ;
#30948=ADVANCED_FACE('',(#2469),#30055,.F.) ;
#30949=ADVANCED_FACE('',(#2470),#1772,.T.) ;
#30950=ADVANCED_FACE('',(#2471),#1773,.T.) ;
#30951=ADVANCED_FACE('',(#2472),#1774,.T.) ;
#30952=ADVANCED_FACE('',(#2473),#1775,.T.) ;
#30953=ADVANCED_FACE('',(#2474),#1776,.T.) ;
#30954=ADVANCED_FACE('',(#2475),#1777,.T.) ;
#30955=ADVANCED_FACE('',(#2476),#1778,.T.) ;
#30956=ADVANCED_FACE('',(#2477),#738,.T.) ;
#30957=ADVANCED_FACE('',(#2478),#739,.T.) ;
#32639=CLOSED_SHELL('',(#30916,#30917,#30918,#30919,#30920,#30921,#30922,
#30923,#30924,#30925,#30926,#30927,#30928,#30929,#30930,#30931,#30932,#30933,
#30934,#30935,#30936,#30937,#30938,#30939,#30940,#30941,#30942,#30943,#30944,
#30945,#30946,#30947,#30948,#30949,#30950,#30951,#30952,#30953,#30954,#30955,
#30956,#30957)) ;
#33124=AXIS2_PLACEMENT_3D('',#48635,#37456,#37457) ;
#33125=AXIS2_PLACEMENT_3D('',#48636,#37458,#37459) ;
#33126=AXIS2_PLACEMENT_3D('',#48647,#37461,#37462) ;
#33127=AXIS2_PLACEMENT_3D('',#48648,#37463,#37464) ;
#33128=AXIS2_PLACEMENT_3D('',#48689,#37466,#37467) ;
#33129=AXIS2_PLACEMENT_3D('',#48724,#37468,#37469) ;
#33130=AXIS2_PLACEMENT_3D('',#48800,#37471,#37472) ;
#33131=AXIS2_PLACEMENT_3D('',#48876,#37474,#37475) ;
#33132=AXIS2_PLACEMENT_3D('',#48952,#37477,#37478) ;
#33133=AXIS2_PLACEMENT_3D('',#49028,#37480,#37481) ;
#33134=AXIS2_PLACEMENT_3D('',#49056,#37483,#37484) ;
#33135=AXIS2_PLACEMENT_3D('',#49060,#37486,#37487) ;
#33136=AXIS2_PLACEMENT_3D('',#49061,#37488,#37489) ;
#33137=AXIS2_PLACEMENT_3D('',#49063,#37490,#37491) ;
#33138=AXIS2_PLACEMENT_3D('',#49082,#37492,#37493) ;
#33139=AXIS2_PLACEMENT_3D('',#49158,#37495,#37496) ;
#33140=AXIS2_PLACEMENT_3D('',#49234,#37498,#37499) ;
#33141=AXIS2_PLACEMENT_3D('',#49312,#37501,#37502) ;
#33142=AXIS2_PLACEMENT_3D('',#49390,#37504,#37505) ;
#33143=AXIS2_PLACEMENT_3D('',#49423,#37506,#37507) ;
#33144=AXIS2_PLACEMENT_3D('',#49450,#37508,#37509) ;
#33145=AXIS2_PLACEMENT_3D('',#49489,#37510,#37511) ;
#33146=AXIS2_PLACEMENT_3D('',#49522,#37512,#37513) ;
#33147=AXIS2_PLACEMENT_3D('',#49524,#37514,#37515) ;
#33148=AXIS2_PLACEMENT_3D('',#49526,#37516,#37517) ;
#33149=AXIS2_PLACEMENT_3D('',#49528,#37518,#37519) ;
#33150=AXIS2_PLACEMENT_3D('',#49529,#37520,#37521) ;
#33151=AXIS2_PLACEMENT_3D('',#49530,#37522,#37523) ;
#33152=AXIS2_PLACEMENT_3D('',#49532,#37525,#37526) ;
#33153=AXIS2_PLACEMENT_3D('',#49535,#37527,#37528) ;
#33154=AXIS2_PLACEMENT_3D('',#49545,#37533,#37534) ;
#33155=AXIS2_PLACEMENT_3D('',#49555,#37539,#37540) ;
#33156=AXIS2_PLACEMENT_3D('',#49565,#37545,#37546) ;
#33157=AXIS2_PLACEMENT_3D('',#49573,#37551,#37552) ;
#33158=AXIS2_PLACEMENT_3D('',#49605,#37554,#37555) ;
#33159=AXIS2_PLACEMENT_3D('',#49636,#37556,#37557) ;
#33160=AXIS2_PLACEMENT_3D('',#49641,#37559,#37560) ;
#33161=AXIS2_PLACEMENT_3D('',#49659,#37561,#37562) ;
#33162=AXIS2_PLACEMENT_3D('',#49677,#37563,#37564) ;
#33163=AXIS2_PLACEMENT_3D('',#49695,#37565,#37566) ;
#33164=AXIS2_PLACEMENT_3D('',#49712,#37567,#37568) ;
#33165=AXIS2_PLACEMENT_3D('',#49713,#37569,#37570) ;
#33166=AXIS2_PLACEMENT_3D('',#49714,#37571,#37572) ;
#33167=AXIS2_PLACEMENT_3D('',#49715,#37573,#37574) ;
#33168=AXIS2_PLACEMENT_3D('',#49716,#37575,#37576) ;
#33169=AXIS2_PLACEMENT_3D('',#49717,#37577,#37578) ;
#33170=AXIS2_PLACEMENT_3D('',#49718,#37579,#37580) ;
#33171=AXIS2_PLACEMENT_3D('',#49719,#37581,#37582) ;
#33172=AXIS2_PLACEMENT_3D('',#49720,#37583,#37584) ;
#33173=AXIS2_PLACEMENT_3D('',#49721,#37585,#37586) ;
#33174=AXIS2_PLACEMENT_3D('',#49722,#37587,#37588) ;
#33175=AXIS2_PLACEMENT_3D('',#49725,#37591,#37592) ;
#33176=AXIS2_PLACEMENT_3D('',#49727,#37594,#37595) ;
#33177=AXIS2_PLACEMENT_3D('',#49728,#37596,#37597) ;
#33178=AXIS2_PLACEMENT_3D('',#49730,#37599,#37600) ;
#33179=AXIS2_PLACEMENT_3D('',#49732,#37602,#37603) ;
#33180=AXIS2_PLACEMENT_3D('',#49734,#37605,#37606) ;
#33181=AXIS2_PLACEMENT_3D('',#49735,#37607,#37608) ;
#33182=AXIS2_PLACEMENT_3D('',#49737,#37610,#37611) ;
#33183=AXIS2_PLACEMENT_3D('',#49739,#37613,#37614) ;
#33184=AXIS2_PLACEMENT_3D('',#49741,#37616,#37617) ;
#33185=AXIS2_PLACEMENT_3D('',#49742,#37618,#37619) ;
#33186=AXIS2_PLACEMENT_3D('',#49743,#37620,#37621) ;
#33187=AXIS2_PLACEMENT_3D('',#49744,#37622,#37623) ;
#33188=AXIS2_PLACEMENT_3D('',#49745,#37624,#37625) ;
#33189=AXIS2_PLACEMENT_3D('',#49747,#37627,#37628) ;
#33190=AXIS2_PLACEMENT_3D('',#49749,#37630,#37631) ;
#33191=AXIS2_PLACEMENT_3D('',#49751,#37633,#37634) ;
#33192=AXIS2_PLACEMENT_3D('',#49752,#37635,#37636) ;
#33193=AXIS2_PLACEMENT_3D('',#49753,#37637,#37638) ;
#33194=AXIS2_PLACEMENT_3D('',#49790,#37639,#37640) ;
#37456=DIRECTION('axis',(0.,0.,1.)) ;
#37457=DIRECTION('refdir',(1.,0.,0.)) ;
#37458=DIRECTION('center_axis',(0.,0.,-1.)) ;
#37459=DIRECTION('ref_axis',(-1.03057430466152E-16,1.,0.)) ;
#37460=DIRECTION('',(0.,0.,1.)) ;
#37461=DIRECTION('center_axis',(0.,9.04152290739048E-17,-1.)) ;
#37462=DIRECTION('ref_axis',(-1.03057430466152E-16,1.,9.04152290739048E-17)) ;
#37463=DIRECTION('center_axis',(0.,0.,-1.)) ;
#37464=DIRECTION('ref_axis',(-1.03057430466152E-16,1.,0.)) ;
#37465=DIRECTION('',(0.,0.,1.)) ;
#37466=DIRECTION('center_axis',(0.,9.04152290739048E-17,-1.)) ;
#37467=DIRECTION('ref_axis',(-1.03057430466152E-16,1.,9.04152290739048E-17)) ;
#37468=DIRECTION('center_axis',(0.,0.,-1.)) ;
#37469=DIRECTION('ref_axis',(-1.03057430466152E-16,1.,0.)) ;
#37470=DIRECTION('',(0.,0.,1.)) ;
#37471=DIRECTION('center_axis',(0.,0.,-1.)) ;
#37472=DIRECTION('ref_axis',(-1.03057430466152E-16,1.,0.)) ;
#37473=DIRECTION('',(0.,0.,1.)) ;
#37474=DIRECTION('center_axis',(0.,0.,-1.)) ;
#37475=DIRECTION('ref_axis',(-1.03057430466152E-16,1.,0.)) ;
#37476=DIRECTION('',(0.,0.,1.)) ;
#37477=DIRECTION('center_axis',(0.,0.,-1.)) ;
#37478=DIRECTION('ref_axis',(-1.03057430466152E-16,1.,0.)) ;
#37479=DIRECTION('',(0.,0.,1.)) ;
#37480=DIRECTION('center_axis',(0.,1.42961865771945E-15,-1.)) ;
#37481=DIRECTION('ref_axis',(0.,1.,1.42961865771945E-15)) ;
#37482=DIRECTION('',(0.,-1.42961865771945E-15,1.)) ;
#37483=DIRECTION('center_axis',(0.,-9.04152290739048E-17,1.)) ;
#37484=DIRECTION('ref_axis',(8.88178419700125E-16,1.,9.04152290739048E-17)) ;
#37485=DIRECTION('',(0.,-1.42961865771945E-15,1.)) ;
#37486=DIRECTION('center_axis',(0.,1.42961865771945E-15,-1.)) ;
#37487=DIRECTION('ref_axis',(0.,1.,1.42961865771945E-15)) ;
#37488=DIRECTION('center_axis',(0.,1.42961865771945E-15,-1.)) ;
#37489=DIRECTION('ref_axis',(0.,1.,1.42961865771945E-15)) ;
#37490=DIRECTION('center_axis',(0.,-9.04152290739048E-17,1.)) ;
#37491=DIRECTION('ref_axis',(8.88178419700125E-16,1.,9.04152290739048E-17)) ;
#37492=DIRECTION('center_axis',(0.,1.42961865771945E-15,-1.)) ;
#37493=DIRECTION('ref_axis',(0.,1.,1.42961865771945E-15)) ;
#37494=DIRECTION('',(0.,-1.42961865771945E-15,1.)) ;
#37495=DIRECTION('center_axis',(0.,1.42961865771945E-15,-1.)) ;
#37496=DIRECTION('ref_axis',(0.,1.,1.42961865771945E-15)) ;
#37497=DIRECTION('',(0.,-1.42961865771945E-15,1.)) ;
#37498=DIRECTION('center_axis',(0.,1.42961865771945E-15,-1.)) ;
#37499=DIRECTION('ref_axis',(0.,1.,1.42961865771945E-15)) ;
#37500=DIRECTION('',(0.,-1.42961865771945E-15,1.)) ;
#37501=DIRECTION('center_axis',(0.,1.42961865771945E-15,-1.)) ;
#37502=DIRECTION('ref_axis',(0.,1.,1.42961865771945E-15)) ;
#37503=DIRECTION('',(0.,-1.42961865771945E-15,1.)) ;
#37504=DIRECTION('center_axis',(0.,1.42961865771945E-15,-1.)) ;
#37505=DIRECTION('ref_axis',(0.,1.,1.42961865771945E-15)) ;
#37506=DIRECTION('center_axis',(0.,1.42961865771945E-15,-1.)) ;
#37507=DIRECTION('ref_axis',(0.,1.,1.42961865771945E-15)) ;
#37508=DIRECTION('center_axis',(0.,0.,-1.)) ;
#37509=DIRECTION('ref_axis',(-1.03057430466152E-16,1.,0.)) ;
#37510=DIRECTION('center_axis',(1.12004190703271E-15,-3.6645376121857E-15,
-1.)) ;
#37511=DIRECTION('ref_axis',(0.104117265609716,-0.99456502804088,3.76123665374887E-15)) ;
#37512=DIRECTION('center_axis',(0.,-1.42652275615057E-16,1.)) ;
#37513=DIRECTION('ref_axis',(1.,0.,0.)) ;
#37514=DIRECTION('center_axis',(0.,1.42652275615057E-16,-1.)) ;
#37515=DIRECTION('ref_axis',(1.22464679914735E-16,1.,1.42652275615057E-16)) ;
#37516=DIRECTION('center_axis',(1.22464679914735E-16,-1.,-1.42652275615057E-16)) ;
#37517=DIRECTION('ref_axis',(-1.,-1.22464679914735E-16,0.)) ;
#37518=DIRECTION('center_axis',(-4.11797682050993E-32,-2.13305428978351E-16,
1.)) ;
#37519=DIRECTION('ref_axis',(0.,1.,2.13305428978351E-16)) ;
#37520=DIRECTION('center_axis',(-4.11797682050993E-32,-2.13305428978351E-16,
1.)) ;
#37521=DIRECTION('ref_axis',(0.,1.,2.13305428978351E-16)) ;
#37522=DIRECTION('center_axis',(0.,-1.42652275615057E-16,1.)) ;
#37523=DIRECTION('ref_axis',(0.,-1.,-1.42652275615057E-16)) ;
#37524=DIRECTION('',(8.03440589904947E-17,-0.656059028990509,-0.754709580222771)) ;
#37525=DIRECTION('center_axis',(0.,1.42652275615057E-16,-1.)) ;
#37526=DIRECTION('ref_axis',(0.,1.,1.42652275615057E-16)) ;
#37527=DIRECTION('center_axis',(0.,0.,1.)) ;
#37528=DIRECTION('ref_axis',(1.,0.,0.)) ;
#37529=DIRECTION('',(-1.,3.18158468314499E-15,0.)) ;
#37530=DIRECTION('',(-0.923879532511288,-0.382683432365087,0.)) ;
#37531=DIRECTION('',(-0.382683432365093,-0.923879532511286,0.)) ;
#37532=DIRECTION('',(3.33653301099406E-15,1.,0.)) ;
#37533=DIRECTION('center_axis',(0.,0.,1.)) ;
#37534=DIRECTION('ref_axis',(-3.49148133884313E-15,-1.,0.)) ;
#37535=DIRECTION('',(-3.09896655698145E-16,1.,0.)) ;
#37536=DIRECTION('',(-0.38268343236509,0.923879532511287,0.)) ;
#37537=DIRECTION('',(-0.923879532511287,0.382683432365089,0.)) ;
#37538=DIRECTION('',(1.,1.54948327849072E-16,0.)) ;
#37539=DIRECTION('center_axis',(0.,0.,1.)) ;
#37540=DIRECTION('ref_axis',(-1.,0.,0.)) ;
#37541=DIRECTION('',(1.,-1.01645473608313E-14,0.)) ;
#37542=DIRECTION('',(0.923879532511291,0.382683432365081,0.)) ;
#37543=DIRECTION('',(0.382683432365099,0.923879532511283,0.)) ;
#37544=DIRECTION('',(-1.03194956886803E-14,-1.,0.)) ;
#37545=DIRECTION('center_axis',(0.,0.,-1.)) ;
#37546=DIRECTION('ref_axis',(1.,-2.66453525910038E-15,0.)) ;
#37547=DIRECTION('',(3.09896655698145E-16,-1.,0.)) ;
#37548=DIRECTION('',(0.38268343236509,-0.923879532511287,0.)) ;
#37549=DIRECTION('',(0.923879532511287,-0.382683432365089,0.)) ;
#37550=DIRECTION('',(-1.,-1.54948327849072E-16,0.)) ;
#37551=DIRECTION('center_axis',(0.,-1.42961865771945E-15,1.)) ;
#37552=DIRECTION('ref_axis',(0.,-1.,-1.42961865771945E-15)) ;
#37553=DIRECTION('',(8.65956056235495E-17,-0.707106781186548,-0.707106781186547)) ;
#37554=DIRECTION('center_axis',(0.,1.42961865771945E-15,-1.)) ;
#37555=DIRECTION('ref_axis',(0.,1.,1.42961865771945E-15)) ;
#37556=DIRECTION('center_axis',(0.,-1.42652275615057E-16,1.)) ;
#37557=DIRECTION('ref_axis',(0.,-1.,-1.42652275615057E-16)) ;
#37558=DIRECTION('',(-8.03440589904947E-17,0.656059028990508,0.754709580222771)) ;
#37559=DIRECTION('center_axis',(0.,-1.42652275615057E-16,1.)) ;
#37560=DIRECTION('ref_axis',(0.,-1.,-1.42652275615057E-16)) ;
#37561=DIRECTION('center_axis',(0.,-1.42652275615057E-16,-1.)) ;
#37562=DIRECTION('ref_axis',(0.,1.,-1.42652275615057E-16)) ;
#37563=DIRECTION('center_axis',(1.42652275615057E-16,-4.9806775825348E-31,
-1.)) ;
#37564=DIRECTION('ref_axis',(-1.,3.49148133884313E-15,-1.42652275615057E-16)) ;
#37565=DIRECTION('center_axis',(0.,1.42652275615057E-16,-1.)) ;
#37566=DIRECTION('ref_axis',(0.,-1.,-1.42652275615057E-16)) ;
#37567=DIRECTION('center_axis',(0.,-1.42652275615057E-16,1.)) ;
#37568=DIRECTION('ref_axis',(0.,-1.,-1.42652275615057E-16)) ;
#37569=DIRECTION('center_axis',(0.,0.,1.)) ;
#37570=DIRECTION('ref_axis',(1.,0.,0.)) ;
#37571=DIRECTION('center_axis',(-3.16947779287894E-15,-0.996194698091746,
-0.0871557427476585)) ;
#37572=DIRECTION('ref_axis',(2.97883628356478E-31,0.0871557427476584,-0.996194698091746)) ;
#37573=DIRECTION('center_axis',(1.54358702681427E-16,-0.996194698091746,
0.0871557427476582)) ;
#37574=DIRECTION('ref_axis',(2.57763828956271E-33,0.0871557427476582,0.996194698091746)) ;
#37575=DIRECTION('center_axis',(0.,0.,1.)) ;
#37576=DIRECTION('ref_axis',(-1.,0.,0.)) ;
#37577=DIRECTION('center_axis',(1.01258681893625E-14,0.996194698091746,
-0.0871557427476582)) ;
#37578=DIRECTION('ref_axis',(7.19854450834723E-33,-0.0871557427476582,-0.996194698091746)) ;
#37579=DIRECTION('center_axis',(-1.54358702681427E-16,0.996194698091746,
0.0871557427476585)) ;
#37580=DIRECTION('ref_axis',(1.2014865513381E-32,-0.0871557427476584,0.996194698091746)) ;
#37581=DIRECTION('center_axis',(0.,0.,1.)) ;
#37582=DIRECTION('ref_axis',(-3.49148133884313E-15,-1.,0.)) ;
#37583=DIRECTION('center_axis',(-0.996194698091746,-3.08717405362855E-16,
-0.0871557427476584)) ;
#37584=DIRECTION('ref_axis',(0.0871557427476584,-3.04302649376462E-16,-0.996194698091746)) ;
#37585=DIRECTION('center_axis',(-0.996194698091746,3.32383649556037E-15,
0.0871557427476584)) ;
#37586=DIRECTION('ref_axis',(0.0871557427476584,-3.04302649376462E-16,0.996194698091746)) ;
#37587=DIRECTION('center_axis',(-0.381227206369651,0.920363891963225,0.0871557427476585)) ;
#37588=DIRECTION('ref_axis',(-0.923879532511288,-0.382683432365087,-7.3858143488638E-17)) ;
#37589=DIRECTION('',(0.0666626913468322,-0.0666626913468327,0.995546167269401)) ;
#37590=DIRECTION('',(0.01733375049386,-0.0871426484044399,0.996045029063886)) ;
#37591=DIRECTION('center_axis',(-0.920363891963223,0.381227206369656,0.0871557427476584)) ;
#37592=DIRECTION('ref_axis',(-0.382683432365092,-0.923879532511286,3.73934789043068E-19)) ;
#37593=DIRECTION('',(0.0871426484044396,-0.0173337504938607,0.996045029063886)) ;
#37594=DIRECTION('center_axis',(-0.996194698091746,3.32383649556037E-15,
0.0871557427476584)) ;
#37595=DIRECTION('ref_axis',(0.0871557427476584,1.34784482901355E-31,0.996194698091746)) ;
#37596=DIRECTION('center_axis',(0.996194698091746,3.08717405362855E-16,
0.0871557427476584)) ;
#37597=DIRECTION('ref_axis',(0.0871557427476584,1.72317352807894E-33,-0.996194698091746)) ;
#37598=DIRECTION('',(-0.0871426484044397,-0.0173337504938605,0.996045029063886)) ;
#37599=DIRECTION('center_axis',(0.920363891963224,0.381227206369654,0.0871557427476584)) ;
#37600=DIRECTION('ref_axis',(-0.38268343236509,0.923879532511287,-7.85426484421263E-17)) ;
#37601=DIRECTION('',(-0.0666626913468323,-0.0666626913468325,0.995546167269401)) ;
#37602=DIRECTION('center_axis',(0.381227206369653,0.920363891963225,0.0871557427476585)) ;
#37603=DIRECTION('ref_axis',(-0.923879532511287,0.382683432365089,1.29793781600155E-17)) ;
#37604=DIRECTION('',(-0.0173337504938602,-0.0871426484044398,0.996045029063886)) ;
#37605=DIRECTION('center_axis',(-1.54358702681427E-16,0.996194698091746,
0.0871557427476585)) ;
#37606=DIRECTION('ref_axis',(-3.11086130697268E-34,-0.0871557427476585,
0.996194698091746)) ;
#37607=DIRECTION('center_axis',(-1.01258681893625E-14,-0.996194698091746,
0.0871557427476582)) ;
#37608=DIRECTION('ref_axis',(-9.14090686442792E-32,-0.0871557427476582,
-0.996194698091746)) ;
#37609=DIRECTION('',(-0.0173337504938594,0.0871426484044397,0.996045029063886)) ;
#37610=DIRECTION('center_axis',(0.381227206369644,-0.920363891963228,0.0871557427476582)) ;
#37611=DIRECTION('ref_axis',(0.923879532511291,0.38268343236508,5.52490330052255E-18)) ;
#37612=DIRECTION('',(-0.0666626913468317,0.0666626913468329,0.995546167269401)) ;
#37613=DIRECTION('center_axis',(0.920363891963221,-0.381227206369663,0.0871557427476583)) ;
#37614=DIRECTION('ref_axis',(0.382683432365099,0.923879532511283,2.18567384430039E-17)) ;
#37615=DIRECTION('',(-0.0871426484044395,0.017333750493861,0.996045029063886)) ;
#37616=DIRECTION('center_axis',(0.996194698091746,-1.0280226892044E-14,
0.0871557427476584)) ;
#37617=DIRECTION('ref_axis',(0.0871557427476584,3.23428151084849E-31,-0.996194698091746)) ;
#37618=DIRECTION('center_axis',(0.996194698091746,-1.0280226892044E-14,
0.0871557427476584)) ;
#37619=DIRECTION('ref_axis',(0.0871557427476584,3.23428151084849E-31,-0.996194698091746)) ;
#37620=DIRECTION('center_axis',(0.,0.,1.)) ;
#37621=DIRECTION('ref_axis',(1.,0.,0.)) ;
#37622=DIRECTION('center_axis',(0.996194698091746,3.08717405362855E-16,
-0.0871557427476584)) ;
#37623=DIRECTION('ref_axis',(0.0871557427476584,-1.34658839111257E-33,0.996194698091746)) ;
#37624=DIRECTION('center_axis',(-0.996194698091746,-3.08717405362855E-16,
0.0871557427476584)) ;
#37625=DIRECTION('ref_axis',(0.0871557427476584,1.72317352807894E-33,0.996194698091746)) ;
#37626=DIRECTION('',(0.0871426484044397,0.0173337504938602,0.996045029063886)) ;
#37627=DIRECTION('center_axis',(-0.920363891963224,-0.381227206369654,0.0871557427476583)) ;
#37628=DIRECTION('ref_axis',(0.38268343236509,-0.923879532511287,-8.49630232542324E-17)) ;
#37629=DIRECTION('',(0.0666626913468323,0.0666626913468322,0.995546167269401)) ;
#37630=DIRECTION('center_axis',(-0.381227206369653,-0.920363891963225,0.0871557427476582)) ;
#37631=DIRECTION('ref_axis',(0.923879532511287,-0.382683432365089,1.74631953898462E-17)) ;
#37632=DIRECTION('',(0.0173337504938602,0.0871426484044396,0.996045029063886)) ;
#37633=DIRECTION('center_axis',(1.54358702681427E-16,-0.996194698091746,
0.0871557427476582)) ;
#37634=DIRECTION('ref_axis',(-1.03689433405292E-33,-0.0871557427476582,
-0.996194698091746)) ;
#37635=DIRECTION('center_axis',(3.16947779287894E-15,0.996194698091746,
0.0871557427476585)) ;
#37636=DIRECTION('ref_axis',(-5.1364595474912E-32,-0.0871557427476585,0.996194698091746)) ;
#37637=DIRECTION('center_axis',(0.,9.04152290739048E-17,-1.)) ;
#37638=DIRECTION('ref_axis',(0.,1.,9.04152290739048E-17)) ;
#37639=DIRECTION('center_axis',(0.,1.42961865771945E-15,-1.)) ;
#37640=DIRECTION('ref_axis',(0.,1.,1.42961865771945E-15)) ;
#48635=CARTESIAN_POINT('',(0.,0.,0.)) ;
#48636=CARTESIAN_POINT('Origin',(1.04083408558609E-16,-6.38378239159465E-15,
-4.1322625)) ;
#48637=CARTESIAN_POINT('',(7.23560708836202E-13,-1.00995540144768,-0.0444499999998741)) ;
#48638=CARTESIAN_POINT('',(8.448295215077E-17,-1.00995540144768,2.72004641033163E-14)) ;
#48639=CARTESIAN_POINT('',(8.448295215077E-17,-1.00995540144768,-4.1322625)) ;
#48640=CARTESIAN_POINT('',(0.433387415541736,-0.912241887310266,2.49185368278523E-14)) ;
#48641=CARTESIAN_POINT('Ctrl Pts',(1.44703693472025E-12,-1.00995540144768,
-0.0444499999998741)) ;
#48642=CARTESIAN_POINT('Ctrl Pts',(0.025506828532912,-1.00995540144768,
-0.0421352325163382)) ;
#48643=CARTESIAN_POINT('Ctrl Pts',(0.0510333004963693,-1.00898920656169,
-0.0397680585416139)) ;
#48644=CARTESIAN_POINT('Ctrl Pts',(0.200353389061228,-0.997642142274717,
-0.0256225970302299)) ;
#48645=CARTESIAN_POINT('Ctrl Pts',(0.321325408922422,-0.965480248872855,
-0.0129591540149241)) ;
#48646=CARTESIAN_POINT('Ctrl Pts',(0.433387415541733,-0.912241887310264,
2.6701731103973E-14)) ;
#48647=CARTESIAN_POINT('Origin',(1.04083408558609E-16,-6.38378239159465E-15,
0.)) ;
#48648=CARTESIAN_POINT('Origin',(1.04083408558609E-16,-6.38378239159465E-15,
-4.1322625)) ;
#48649=CARTESIAN_POINT('',(6.357143120128E-13,-1.00995540144768,-0.679449999999891)) ;
#48650=CARTESIAN_POINT('',(2.45193363101085E-13,-1.00995540144768,-0.600074999999959)) ;
#48651=CARTESIAN_POINT('',(8.448295215077E-17,-1.00995540144768,-4.1322625)) ;
#48652=CARTESIAN_POINT('Ctrl Pts',(1.27134414107345E-12,-1.00995540144768,
-0.679449999999891)) ;
#48653=CARTESIAN_POINT('Ctrl Pts',(0.0437634009185802,-1.00995540144768,
-0.675478432257258)) ;
#48654=CARTESIAN_POINT('Ctrl Pts',(0.0875582439193204,-1.00711177961309,
-0.671355019401001)) ;
#48655=CARTESIAN_POINT('Ctrl Pts',(0.26557918047378,-0.983801453112301,
-0.653978114529555)) ;
#48656=CARTESIAN_POINT('Ctrl Pts',(0.395064237667927,-0.939304962798357,
-0.639895833911083)) ;
#48657=CARTESIAN_POINT('Ctrl Pts',(0.624303148323518,-0.804528605296291,
-0.612030583529934)) ;
#48658=CARTESIAN_POINT('Ctrl Pts',(0.72291777299032,-0.71724247121487,-0.598507856602888)) ;
#48659=CARTESIAN_POINT('Ctrl Pts',(0.881958923219596,-0.509301855514422,
-0.57317967053573)) ;
#48660=CARTESIAN_POINT('Ctrl Pts',(0.940594127778358,-0.390554680687541,
-0.56162626629538)) ;
#48661=CARTESIAN_POINT('Ctrl Pts',(1.00987101600572,-0.134547391647658,
-0.534799235400863)) ;
#48662=CARTESIAN_POINT('Ctrl Pts',(1.01878989490851,0.000372688306628111,
-0.520660945952939)) ;
#48663=CARTESIAN_POINT('Ctrl Pts',(0.984171959584064,0.260795586207613,
-0.49337120293886)) ;
#48664=CARTESIAN_POINT('Ctrl Pts',(0.942902939882405,0.384163694667602,
-0.48044344580559)) ;
#48665=CARTESIAN_POINT('Ctrl Pts',(0.813570221399235,0.613266917555062,
-0.456435694848632)) ;
#48666=CARTESIAN_POINT('Ctrl Pts',(0.724956102393718,0.715905786899936,
-0.443147159257415)) ;
#48667=CARTESIAN_POINT('Ctrl Pts',(0.514163423924961,0.879282972696947,
-0.415457379020839)) ;
#48668=CARTESIAN_POINT('Ctrl Pts',(0.394709115734629,0.938997134833771,
-0.401488067118609)) ;
#48669=CARTESIAN_POINT('Ctrl Pts',(0.143188392677125,1.00798005112781,-0.375047973181057)) ;
#48670=CARTESIAN_POINT('Ctrl Pts',(0.0140058409597491,1.01799616298282,
-0.363642338709345)) ;
#48671=CARTESIAN_POINT('Ctrl Pts',(-0.247226330001402,0.988414461209624,
-0.338385350914255)) ;
#48672=CARTESIAN_POINT('Ctrl Pts',(-0.37639700835342,0.946773140710743,
-0.324481197230098)) ;
#48673=CARTESIAN_POINT('Ctrl Pts',(-0.607610842133004,0.817251073521645,
-0.296712019629347)) ;
#48674=CARTESIAN_POINT('Ctrl Pts',(-0.708196666452128,0.731827505295378,
-0.283107993808755)) ;
#48675=CARTESIAN_POINT('Ctrl Pts',(-0.871156333072791,0.527411858369104,
-0.257608889802603)) ;
#48676=CARTESIAN_POINT('Ctrl Pts',(-0.931970985059438,0.41050304059754,
-0.246216657040143)) ;
#48677=CARTESIAN_POINT('Ctrl Pts',(-1.0067530655191,0.156419528956202,-0.219591218982685)) ;
#48678=CARTESIAN_POINT('Ctrl Pts',(-1.01860033273544,0.0214369986454144,
-0.205446385355298)) ;
#48679=CARTESIAN_POINT('Ctrl Pts',(-0.989435466647989,-0.240200133406872,
-0.178029402616084)) ;
#48680=CARTESIAN_POINT('Ctrl Pts',(-0.950651931827455,-0.364659436823405,
-0.164987299047911)) ;
#48681=CARTESIAN_POINT('Ctrl Pts',(-0.825247524122355,-0.597764147034261,
-0.140560231811127)) ;
#48682=CARTESIAN_POINT('Ctrl Pts',(-0.737680683582466,-0.703030138026511,
-0.127476546675298)) ;
#48683=CARTESIAN_POINT('Ctrl Pts',(-0.528466085007257,-0.870794003954716,
-0.0997001382618737)) ;
#48684=CARTESIAN_POINT('Ctrl Pts',(-0.4098063543708,-0.932536041247264,
-0.0856966843567157)) ;
#48685=CARTESIAN_POINT('Ctrl Pts',(-0.190611916996757,-0.996422885426864,
-0.0624572387014332)) ;
#48686=CARTESIAN_POINT('Ctrl Pts',(-0.0955075072374286,-1.00995540144768,
-0.0531173916325512)) ;
#48687=CARTESIAN_POINT('Ctrl Pts',(1.44703693472025E-12,-1.00995540144768,
-0.0444499999998741)) ;
#48688=CARTESIAN_POINT('',(-0.348937280953797,-0.94776193575914,-1.56815741427684E-16)) ;
#48689=CARTESIAN_POINT('Origin',(1.04083408558609E-16,-6.38378239159465E-15,
0.)) ;
#48690=CARTESIAN_POINT('Ctrl Pts',(-0.348937280953794,-0.947761935759138,
-2.01878444516801E-15)) ;
#48691=CARTESIAN_POINT('Ctrl Pts',(-0.461713552528522,-0.906241123332891,
-0.0124100325913252)) ;
#48692=CARTESIAN_POINT('Ctrl Pts',(-0.566180329108771,-0.844921873509237,
-0.0251033112604733)) ;
#48693=CARTESIAN_POINT('Ctrl Pts',(-0.745859616028041,-0.690852949413873,
-0.0494818165451801)) ;
#48694=CARTESIAN_POINT('Ctrl Pts',(-0.820397680576272,-0.600383170618035,
-0.0609107840527787)) ;
#48695=CARTESIAN_POINT('Ctrl Pts',(-0.94161187970814,-0.387303216910876,
-0.0832394549376677)) ;
#48696=CARTESIAN_POINT('Ctrl Pts',(-0.983280258010021,-0.264116309328272,
-0.0961482240118311)) ;
#48697=CARTESIAN_POINT('Ctrl Pts',(-1.01877670334187,-0.00390044213731634,
-0.123416272255909)) ;
#48698=CARTESIAN_POINT('Ctrl Pts',(-1.01033073852162,0.131003656243038,
-0.137552886993011)) ;
#48699=CARTESIAN_POINT('Ctrl Pts',(-0.941947087402141,0.387317636260553,
-0.164412056067511)) ;
#48700=CARTESIAN_POINT('Ctrl Pts',(-0.883664649499574,0.506364361030241,
-0.175995964172646)) ;
#48701=CARTESIAN_POINT('Ctrl Pts',(-0.725256301987552,0.714870181751489,
-0.201296336774658)) ;
#48702=CARTESIAN_POINT('Ctrl Pts',(-0.626961756250327,0.802451546689399,
-0.214805484889144)) ;
#48703=CARTESIAN_POINT('Ctrl Pts',(-0.398251277024382,0.937951740403398,
-0.242660705082419)) ;
#48704=CARTESIAN_POINT('Ctrl Pts',(-0.268963099837451,0.982875339591604,
-0.256747497056347)) ;
#48705=CARTESIAN_POINT('Ctrl Pts',(-0.00710515020264792,1.01809280298334,
-0.282356560853332)) ;
#48706=CARTESIAN_POINT('Ctrl Pts',(0.122441064791949,1.0107326518681,-0.293645911973156)) ;
#48707=CARTESIAN_POINT('Ctrl Pts',(0.375235433236055,0.946911055779092,
-0.319931162722662)) ;
#48708=CARTESIAN_POINT('Ctrl Pts',(0.495656691472225,0.889806436177891,
-0.333851499086522)) ;
#48709=CARTESIAN_POINT('Ctrl Pts',(0.709442571371163,0.731236512440977,
-0.361561038277925)) ;
#48710=CARTESIAN_POINT('Ctrl Pts',(0.800277276817402,0.630566775295668,
-0.375078965173411)) ;
#48711=CARTESIAN_POINT('Ctrl Pts',(0.934302509181679,0.404472785875835,
-0.399088081314702)) ;
#48712=CARTESIAN_POINT('Ctrl Pts',(0.978213313024649,0.282309921238749,
-0.411741713495526)) ;
#48713=CARTESIAN_POINT('Ctrl Pts',(1.01849267055767,0.0230223918801653,
-0.438912481119966)) ;
#48714=CARTESIAN_POINT('Ctrl Pts',(1.01260644401027,-0.111766631062521,
-0.453037037089784)) ;
#48715=CARTESIAN_POINT('Ctrl Pts',(0.949079392935516,-0.369721482521146,
-0.480068153256141)) ;
#48716=CARTESIAN_POINT('Ctrl Pts',(0.892711807051305,-0.490402608322398,
-0.491838609662575)) ;
#48717=CARTESIAN_POINT('Ctrl Pts',(0.737729733608816,-0.701949266681669,
-0.516987369679715)) ;
#48718=CARTESIAN_POINT('Ctrl Pts',(0.641175934951445,-0.791102258115751,
-0.530420888894451)) ;
#48719=CARTESIAN_POINT('Ctrl Pts',(0.415352993918571,-0.93047025311943,
-0.558216716069348)) ;
#48720=CARTESIAN_POINT('Ctrl Pts',(0.287149755951262,-0.977682389087762,
-0.572324956845148)) ;
#48721=CARTESIAN_POINT('Ctrl Pts',(0.102530413489681,-1.00605547915662,
-0.590565936714243)) ;
#48722=CARTESIAN_POINT('Ctrl Pts',(0.0512545503777301,-1.00995540144768,
-0.595423603749283)) ;
#48723=CARTESIAN_POINT('Ctrl Pts',(4.90302243250019E-13,-1.00995540144768,
-0.600074999999959)) ;
#48724=CARTESIAN_POINT('Origin',(1.04083408558609E-16,-6.38378239159465E-15,
-4.1322625)) ;
#48725=CARTESIAN_POINT('',(7.26230717109419E-14,-1.00995540144768,-1.31444999999999)) ;
#48726=CARTESIAN_POINT('',(-6.18419324832232E-17,-1.00995540144768,-1.235075)) ;
#48727=CARTESIAN_POINT('',(8.448295215077E-17,-1.00995540144768,-4.1322625)) ;
#48728=CARTESIAN_POINT('Ctrl Pts',(1.45161660469733E-13,-1.00995540144768,
-1.31444999999999)) ;
#48729=CARTESIAN_POINT('Ctrl Pts',(0.0565109964714736,-1.00995540144768,
-1.30932157656885)) ;
#48730=CARTESIAN_POINT('Ctrl Pts',(0.113028660198271,-1.00521499788339,
-1.30394417438287)) ;
#48731=CARTESIAN_POINT('Ctrl Pts',(0.302193867993356,-0.973108983005214,
-1.28509506637953)) ;
#48732=CARTESIAN_POINT('Ctrl Pts',(0.429465110701191,-0.924012640872624,
-1.2709726819248)) ;
#48733=CARTESIAN_POINT('Ctrl Pts',(0.652838291547309,-0.781473970039967,
-1.24323304494836)) ;
#48734=CARTESIAN_POINT('Ctrl Pts',(0.747925745683043,-0.691040292433543,
-1.22986549618965)) ;
#48735=CARTESIAN_POINT('Ctrl Pts',(0.900039665300462,-0.476973275113707,
-1.20484496935425)) ;
#48736=CARTESIAN_POINT('Ctrl Pts',(0.954797052853043,-0.354908264883124,
-1.19289087461317)) ;
#48737=CARTESIAN_POINT('Ctrl Pts',(1.01423245983247,-0.095605949188269,
-1.16571855752699)) ;
#48738=CARTESIAN_POINT('Ctrl Pts',(1.01797796810863,0.0390496479844164,
-1.15160798325772)) ;
#48739=CARTESIAN_POINT('Ctrl Pts',(0.973735166614192,0.297314907494692,
-1.1245443393988)) ;
#48740=CARTESIAN_POINT('Ctrl Pts',(0.928022939522984,0.418646151519161,
-1.11215059051402)) ;
#48741=CARTESIAN_POINT('Ctrl Pts',(0.790642705724418,0.642609633844796,
-1.08794863302621)) ;
#48742=CARTESIAN_POINT('Ctrl Pts',(0.698279070382183,0.741908739075154,
-1.07436376870799)) ;
#48743=CARTESIAN_POINT('Ctrl Pts',(0.482247866830835,0.897115859201658,
-1.04662665866158)) ;
#48744=CARTESIAN_POINT('Ctrl Pts',(0.361167799952309,0.952339641367629,
-1.03274508140156)) ;
#48745=CARTESIAN_POINT('Ctrl Pts',(0.107478375300796,1.01245532598292,-1.006572774929)) ;
#48746=CARTESIAN_POINT('Ctrl Pts',(-0.0223459833230694,1.01789594597081,
-0.995338127294016)) ;
#48747=CARTESIAN_POINT('Ctrl Pts',(-0.283626891794233,0.978716836240998,
-0.969573859828927)) ;
#48748=CARTESIAN_POINT('Ctrl Pts',(-0.412043838067636,0.931947088196774,
-0.955469403772045)) ;
#48749=CARTESIAN_POINT('Ctrl Pts',(-0.63843240043722,0.793325346866863,
-0.927661345956073)) ;
#48750=CARTESIAN_POINT('Ctrl Pts',(-0.735326105056216,0.704474795907485,
-0.914212826356226)) ;
#48751=CARTESIAN_POINT('Ctrl Pts',(-0.890975285096107,0.493517630963721,
-0.889034412357887)) ;
#48752=CARTESIAN_POINT('Ctrl Pts',(-0.947716387344409,0.373156358605394,
-0.877303094284298)) ;
#48753=CARTESIAN_POINT('Ctrl Pts',(-1.01219170575329,0.115518356801635,
-0.850305180826787)) ;
#48754=CARTESIAN_POINT('Ctrl Pts',(-1.01857616319312,-0.0192968522412743,
-0.836177880812757)) ;
#48755=CARTESIAN_POINT('Ctrl Pts',(-0.979219896892731,-0.278819755610391,
-0.808982448320859)) ;
#48756=CARTESIAN_POINT('Ctrl Pts',(-0.935726541635327,-0.401177227310065,
-0.796264984497799)) ;
#48757=CARTESIAN_POINT('Ctrl Pts',(-0.802479205122599,-0.627761205578296,
-0.772300790108584)) ;
#48758=CARTESIAN_POINT('Ctrl Pts',(-0.712001100701131,-0.728744435673642,
-0.758798799595079)) ;
#48759=CARTESIAN_POINT('Ctrl Pts',(-0.49874208733636,-0.888087400594881,
-0.731096570478756)) ;
#48760=CARTESIAN_POINT('Ctrl Pts',(-0.378477339871019,-0.945625968271003,
-0.717167700874882)) ;
#48761=CARTESIAN_POINT('Ctrl Pts',(-0.168470635591927,-0.999401318650093,
-0.695291842461025)) ;
#48762=CARTESIAN_POINT('Ctrl Pts',(-0.0843440584127307,-1.00995540144768,
-0.687104298675449)) ;
#48763=CARTESIAN_POINT('Ctrl Pts',(1.27134414107345E-12,-1.00995540144768,
-0.679449999999891)) ;
#48764=CARTESIAN_POINT('Ctrl Pts',(4.90302243250019E-13,-1.00995540144768,
-0.600074999999959)) ;
#48765=CARTESIAN_POINT('Ctrl Pts',(-0.0770781742531291,-1.00995540144768,
-0.60706991319485)) ;
#48766=CARTESIAN_POINT('Ctrl Pts',(-0.154023911223334,-1.00114029685864,
-0.614514675458974)) ;
#48767=CARTESIAN_POINT('Ctrl Pts',(-0.357783489255834,-0.953610067886598,
-0.6354963881168)) ;
#48768=CARTESIAN_POINT('Ctrl Pts',(-0.479017160202537,-0.898838236541642,
-0.649368225096111)) ;
#48769=CARTESIAN_POINT('Ctrl Pts',(-0.695578689880959,-0.74444211912628,
-0.677110970182544)) ;
#48770=CARTESIAN_POINT('Ctrl Pts',(-0.788305698603855,-0.645475225111657,
-0.690711404735574)) ;
#48771=CARTESIAN_POINT('Ctrl Pts',(-0.926488213354373,-0.422025397907093,
-0.7149592569495)) ;
#48772=CARTESIAN_POINT('Ctrl Pts',(-0.972631542089144,-0.300891171801688,
-0.727294582283833)) ;
#48773=CARTESIAN_POINT('Ctrl Pts',(-1.01781791392863,-0.0428720573080172,
-0.754332432580429)) ;
#48774=CARTESIAN_POINT('Ctrl Pts',(-1.01458231554768,0.0917467407720381,
-0.768439150668889)) ;
#48775=CARTESIAN_POINT('Ctrl Pts',(-0.956125807533879,0.351366681622582,
-0.79564475172873)) ;
#48776=CARTESIAN_POINT('Ctrl Pts',(-0.901753381462521,0.473763630641837,
-0.80764627858924)) ;
#48777=CARTESIAN_POINT('Ctrl Pts',(-0.750323191744204,0.688428094908377,
-0.832636059589635)) ;
#48778=CARTESIAN_POINT('Ctrl Pts',(-0.655586413466596,0.779162370652702,
-0.845987534056174)) ;
#48779=CARTESIAN_POINT('Ctrl Pts',(-0.432801382336186,0.922447816402019,
-0.873712923231553)) ;
#48780=CARTESIAN_POINT('Ctrl Pts',(-0.305755405079719,0.971989039570837,
-0.887838174210686)) ;
#48781=CARTESIAN_POINT('Ctrl Pts',(-0.0453962757393742,1.01717320061781,
-0.913833424377218)) ;
#48782=CARTESIAN_POINT('Ctrl Pts',(0.0848738524560454,1.01464328987563,
-0.925031755796313)) ;
#48783=CARTESIAN_POINT('Ctrl Pts',(0.339879357290095,0.960104774255783,
-0.951031281657117)) ;
#48784=CARTESIAN_POINT('Ctrl Pts',(0.461894575965491,0.907720518449188,
-0.964848947644651)) ;
#48785=CARTESIAN_POINT('Ctrl Pts',(0.681199070812265,0.757627517530871,
-0.992615157254959)) ;
#48786=CARTESIAN_POINT('Ctrl Pts',(0.775820085330474,0.660433840697432,
-1.00629456671852)) ;
#48787=CARTESIAN_POINT('Ctrl Pts',(0.918217069813966,0.439709332307288,
-1.0307820926036)) ;
#48788=CARTESIAN_POINT('Ctrl Pts',(0.966628035471543,0.319598446430998,
-1.04283424499689)) ;
#48789=CARTESIAN_POINT('Ctrl Pts',(1.01674514418657,0.0628828651013657,
-1.06973549791536)) ;
#48790=CARTESIAN_POINT('Ctrl Pts',(1.01617497448599,-0.0715119915840745,
-1.0838187491614)) ;
#48791=CARTESIAN_POINT('Ctrl Pts',(0.962863906090873,-0.332771271630767,
-1.11119613674899)) ;
#48792=CARTESIAN_POINT('Ctrl Pts',(0.910514170054564,-0.456917853227476,
-1.12346859379693)) ;
#48793=CARTESIAN_POINT('Ctrl Pts',(0.762662596351267,-0.674688186803455,
-1.14829634438262)) ;
#48794=CARTESIAN_POINT('Ctrl Pts',(0.669767552817714,-0.766966274896015,
-1.16156156790488)) ;
#48795=CARTESIAN_POINT('Ctrl Pts',(0.450085565295974,-0.914103075865332,
-1.18920714506014)) ;
#48796=CARTESIAN_POINT('Ctrl Pts',(0.324237320273755,-0.965945585652875,
-1.20334427680273)) ;
#48797=CARTESIAN_POINT('Ctrl Pts',(0.128503467450188,-1.00382548182994,
-1.2230920180285)) ;
#48798=CARTESIAN_POINT('Ctrl Pts',(0.064265873499002,-1.00995540144768,
-1.2292428145484)) ;
#48799=CARTESIAN_POINT('Ctrl Pts',(-2.08166817117216E-16,-1.00995540144768,
-1.235075)) ;
#48800=CARTESIAN_POINT('Origin',(1.04083408558609E-16,-6.38378239159465E-15,
-4.1322625)) ;
#48801=CARTESIAN_POINT('',(-8.02468796914548E-14,-1.00995540144768,-1.94945000000002)) ;
#48802=CARTESIAN_POINT('',(-1.98317215169442E-13,-1.00995540144768,-1.87007500000004)) ;
#48803=CARTESIAN_POINT('',(8.448295215077E-17,-1.00995540144768,-4.1322625)) ;
#48804=CARTESIAN_POINT('Ctrl Pts',(-1.6057824233506E-13,-1.00995540144768,
-1.94945000000002)) ;
#48805=CARTESIAN_POINT('Ctrl Pts',(0.0723553003243024,-1.00995540144769,
-1.94288369183485)) ;
#48806=CARTESIAN_POINT('Ctrl Pts',(0.144623390562603,-1.00218667636261,
-1.93591825530127)) ;
#48807=CARTESIAN_POINT('Ctrl Pts',(0.344225695278461,-0.958562901762504,
-1.9155184977955)) ;
#48808=CARTESIAN_POINT('Ctrl Pts',(0.466055957642379,-0.905599570317038,
-1.90168727605979)) ;
#48809=CARTESIAN_POINT('Ctrl Pts',(0.680797269323851,-0.757160674168711,
-1.87442184630654)) ;
#48810=CARTESIAN_POINT('Ctrl Pts',(0.772221484095825,-0.663690612493028,
-1.86122764828989)) ;
#48811=CARTESIAN_POINT('Ctrl Pts',(0.91722818854932,-0.443476524508156,
-1.83653003148946)) ;
#48812=CARTESIAN_POINT('Ctrl Pts',(0.967959630703487,-0.317925019761586,
-1.82401539644544)) ;
#48813=CARTESIAN_POINT('Ctrl Pts',(1.01715414359895,-0.0553907798653038,
-1.79650440568037)) ;
#48814=CARTESIAN_POINT('Ctrl Pts',(1.01561050663032,0.0787883937661297,
-1.78244375588438)) ;
#48815=CARTESIAN_POINT('Ctrl Pts',(0.961582983560333,0.334449715008675,
-1.75565297899194)) ;
#48816=CARTESIAN_POINT('Ctrl Pts',(0.911354849604406,0.45375657101305,-1.7437983341723)) ;
#48817=CARTESIAN_POINT('Ctrl Pts',(0.765589482467509,0.672269616441594,
-1.71912099427007)) ;
#48818=CARTESIAN_POINT('Ctrl Pts',(0.669473384740545,0.768012341070395,
-1.70538192738671)) ;
#48819=CARTESIAN_POINT('Ctrl Pts',(0.448029690569759,0.914615154714995,
-1.67760445207281)) ;
#48820=CARTESIAN_POINT('Ctrl Pts',(0.32542091582782,0.965075466611859,-1.66383372548469)) ;
#48821=CARTESIAN_POINT('Ctrl Pts',(0.0695471621562103,1.01584437983776,
-1.63795291378274)) ;
#48822=CARTESIAN_POINT('Ctrl Pts',(-0.061042847696245,1.01639061240754,
-1.62674748023882)) ;
#48823=CARTESIAN_POINT('Ctrl Pts',(-0.320741465994523,0.967118688915825,
-1.60059799351017)) ;
#48824=CARTESIAN_POINT('Ctrl Pts',(-0.446819982081549,0.915710520284951,
-1.58646272179053)) ;
#48825=CARTESIAN_POINT('Ctrl Pts',(-0.667095500822319,0.769299116080178,
-1.55880128834857)) ;
#48826=CARTESIAN_POINT('Ctrl Pts',(-0.760341749797416,0.677310961433985,
-1.54551938369688)) ;
#48827=CARTESIAN_POINT('Ctrl Pts',(-0.908874243045885,0.46012886265203,
-1.5206606596471)) ;
#48828=CARTESIAN_POINT('Ctrl Pts',(-0.961609909749135,0.336316743673208,
-1.50844266713929)) ;
#48829=CARTESIAN_POINT('Ctrl Pts',(-1.01590285320031,0.0753663643783231,
-1.48109764929416)) ;
#48830=CARTESIAN_POINT('Ctrl Pts',(-1.01697968853456,-0.0590751536885078,
-1.46700950839704)) ;
#48831=CARTESIAN_POINT('Ctrl Pts',(-0.967799758829855,-0.316040723953939,
-1.44008205911155)) ;
#48832=CARTESIAN_POINT('Ctrl Pts',(-0.919821777225401,-0.436345304729499,
-1.42797897963809)) ;
#48833=CARTESIAN_POINT('Ctrl Pts',(-0.778228666363001,-0.657593182198298,
-1.40353698405195)) ;
#48834=CARTESIAN_POINT('Ctrl Pts',(-0.683966951987112,-0.755128715282229,
-1.38987226982107)) ;
#48835=CARTESIAN_POINT('Ctrl Pts',(-0.465180022352401,-0.90604801038786,
-1.36210973598864)) ;
#48836=CARTESIAN_POINT('Ctrl Pts',(-0.343310564426513,-0.958889388421443,
-1.34828134697613)) ;
#48837=CARTESIAN_POINT('Ctrl Pts',(-0.143990621346624,-1.00225470563842,
-1.32792075592941)) ;
#48838=CARTESIAN_POINT('Ctrl Pts',(-0.072037538307033,-1.00995540144768,
-1.32098747097813)) ;
#48839=CARTESIAN_POINT('Ctrl Pts',(1.45161660469733E-13,-1.00995540144768,
-1.31444999999999)) ;
#48840=CARTESIAN_POINT('Ctrl Pts',(-2.08166817117216E-16,-1.00995540144768,
-1.235075)) ;
#48841=CARTESIAN_POINT('Ctrl Pts',(-0.0646876702990289,-1.00995540144768,
-1.24094546388815)) ;
#48842=CARTESIAN_POINT('Ctrl Pts',(-0.129344610750813,-1.0037448041883,
-1.24713854358703)) ;
#48843=CARTESIAN_POINT('Ctrl Pts',(-0.322043264294838,-0.966201838386248,
-1.26659318428093)) ;
#48844=CARTESIAN_POINT('Ctrl Pts',(-0.444785930738073,-0.916190451953308,
-1.28035254018717)) ;
#48845=CARTESIAN_POINT('Ctrl Pts',(-0.66671972164513,-0.770404905740835,
-1.30813167144754)) ;
#48846=CARTESIAN_POINT('Ctrl Pts',(-0.763180705005661,-0.675003549261792,
-1.3218841510081)) ;
#48847=CARTESIAN_POINT('Ctrl Pts',(-0.909728661768419,-0.457008614310503,
-1.34660536519238)) ;
#48848=CARTESIAN_POINT('Ctrl Pts',(-0.960379737745155,-0.337886824477322,
-1.35841780392719)) ;
#48849=CARTESIAN_POINT('Ctrl Pts',(-1.01531202255019,-0.0824720101177455,
-1.3851827493373)) ;
#48850=CARTESIAN_POINT('Ctrl Pts',(-1.01734459520918,0.0516524552068899,
-1.39923766624404)) ;
#48851=CARTESIAN_POINT('Ctrl Pts',(-0.96910705685852,0.314478405656836,
-1.42677922538887)) ;
#48852=CARTESIAN_POINT('Ctrl Pts',(-0.918751951194141,0.440357074358718,
-1.43935330491219)) ;
#48853=CARTESIAN_POINT('Ctrl Pts',(-0.77440432267991,0.661134117077949,
-1.46402060602521)) ;
#48854=CARTESIAN_POINT('Ctrl Pts',(-0.683321601246241,0.754875873315237,
-1.47719804866716)) ;
#48855=CARTESIAN_POINT('Ctrl Pts',(-0.466715554991479,0.905690194324463,
-1.50475716526057)) ;
#48856=CARTESIAN_POINT('Ctrl Pts',(-0.342069221262696,0.959741291666654,
-1.51890094154091)) ;
#48857=CARTESIAN_POINT('Ctrl Pts',(-0.083356074104296,1.01486601437281,
-1.54526765360729)) ;
#48858=CARTESIAN_POINT('Ctrl Pts',(0.0476993612733256,1.01716462966343,
-1.55652603176877)) ;
#48859=CARTESIAN_POINT('Ctrl Pts',(0.30478503753594,0.971753598811276,-1.5822360999986)) ;
#48860=CARTESIAN_POINT('Ctrl Pts',(0.428184010449668,0.924032903527723,
-1.59593499541964)) ;
#48861=CARTESIAN_POINT('Ctrl Pts',(0.65256564006348,0.782434360912067,-1.6237168919553)) ;
#48862=CARTESIAN_POINT('Ctrl Pts',(0.750763187048053,0.688791284702509,
-1.63753484102893)) ;
#48863=CARTESIAN_POINT('Ctrl Pts',(0.901285507204505,0.473453138348931,
-1.66247752966383)) ;
#48864=CARTESIAN_POINT('Ctrl Pts',(0.954089680485891,0.355261282001321,
-1.67409713268568)) ;
#48865=CARTESIAN_POINT('Ctrl Pts',(1.01359551140853,0.101107455485839,-1.70072993904624)) ;
#48866=CARTESIAN_POINT('Ctrl Pts',(1.01809809795569,-0.0327128628235703,
-1.71475298435508)) ;
#48867=CARTESIAN_POINT('Ctrl Pts',(0.97472400106394,-0.296993875268589,
-1.74244701960028)) ;
#48868=CARTESIAN_POINT('Ctrl Pts',(0.926282905700387,-0.424537957414063,
-1.75534102059181)) ;
#48869=CARTESIAN_POINT('Ctrl Pts',(0.785271774586696,-0.648146462177879,
-1.77985388618761)) ;
#48870=CARTESIAN_POINT('Ctrl Pts',(0.695921543177911,-0.743238012536047,
-1.7929448263459)) ;
#48871=CARTESIAN_POINT('Ctrl Pts',(0.482275975299125,-0.897467842237503,
-1.82041423263958)) ;
#48872=CARTESIAN_POINT('Ctrl Pts',(0.358799392659723,-0.953580438943742,
-1.8345598653314)) ;
#48873=CARTESIAN_POINT('Ctrl Pts',(0.153004812027378,-1.00125741452764,
-1.85573394509024)) ;
#48874=CARTESIAN_POINT('Ctrl Pts',(0.0765634856563495,-1.00995540144771,
-1.86312679525529)) ;
#48875=CARTESIAN_POINT('Ctrl Pts',(-3.96718913291035E-13,-1.00995540144768,
-1.87007500000004)) ;
#48876=CARTESIAN_POINT('Origin',(1.04083408558609E-16,-6.38378239159465E-15,
-4.1322625)) ;
#48877=CARTESIAN_POINT('',(-6.5243389008471E-13,-1.00995540144768,-2.58445000000013)) ;
#48878=CARTESIAN_POINT('',(-7.96237503807855E-13,-1.00995540144768,-2.50507500000015)) ;
#48879=CARTESIAN_POINT('',(8.448295215077E-17,-1.00995540144768,-4.1322625)) ;
#48880=CARTESIAN_POINT('Ctrl Pts',(-1.30495226312157E-12,-1.00995540144768,
-2.58445000000013)) ;
#48881=CARTESIAN_POINT('Ctrl Pts',(0.0846470609818248,-1.00995540144779,
-2.57676820357058)) ;
#48882=CARTESIAN_POINT('Ctrl Pts',(0.169072699863829,-0.999325393833233,
-2.56854954158348)) ;
#48883=CARTESIAN_POINT('Ctrl Pts',(0.379335907038639,-0.945283480371864,
-2.54663643871582)) ;
#48884=CARTESIAN_POINT('Ctrl Pts',(0.499558908636285,-0.88762995657192,
-2.53270533445456)) ;
#48885=CARTESIAN_POINT('Ctrl Pts',(0.712677793878948,-0.728082385899932,
-2.50500510176141)) ;
#48886=CARTESIAN_POINT('Ctrl Pts',(0.80306118939936,-0.627016282211641,
-2.49150736399903)) ;
#48887=CARTESIAN_POINT('Ctrl Pts',(0.936102208690891,-0.400302596724463,
-2.46755509706542)) ;
#48888=CARTESIAN_POINT('Ctrl Pts',(0.979484856296888,-0.277893397385756,
-2.45482047850282)) ;
#48889=CARTESIAN_POINT('Ctrl Pts',(1.0185960320577,-0.0183081726476704,
-2.42761851534808)) ;
#48890=CARTESIAN_POINT('Ctrl Pts',(1.01207931533077,0.11651367972252,-2.41349051917908)) ;
#48891=CARTESIAN_POINT('Ctrl Pts',(0.947352518855438,0.374067365839076,
-2.38650144117135)) ;
#48892=CARTESIAN_POINT('Ctrl Pts',(0.890512334711962,0.494343871604385,
-2.37478028355899)) ;
#48893=CARTESIAN_POINT('Ctrl Pts',(0.734686087275951,0.70514436145921,-2.34959400953578)) ;
#48894=CARTESIAN_POINT('Ctrl Pts',(0.637702239542249,0.793914347644846,
-2.3361415305633)) ;
#48895=CARTESIAN_POINT('Ctrl Pts',(0.411163818275492,0.932337458834412,
-2.30833028015519)) ;
#48896=CARTESIAN_POINT('Ctrl Pts',(0.282690346142352,0.978989524863807,
-2.29422686028141)) ;
#48897=CARTESIAN_POINT('Ctrl Pts',(0.0213717919190553,1.01791521876209,
-2.26847245416657)) ;
#48898=CARTESIAN_POINT('Ctrl Pts',(-0.108434393691808,1.01235181018582,
-2.25723504183201)) ;
#48899=CARTESIAN_POINT('Ctrl Pts',(-0.362067206439329,0.95199970886247,
-2.23105548587441)) ;
#48900=CARTESIAN_POINT('Ctrl Pts',(-0.483106134822916,0.896655782819292,
-2.21717134702477)) ;
#48901=CARTESIAN_POINT('Ctrl Pts',(-0.698995761555616,0.741233261904337,
-2.18943579926547)) ;
#48902=CARTESIAN_POINT('Ctrl Pts',(-0.791262538823597,0.641846029332726,
-2.17585510746734)) ;
#48903=CARTESIAN_POINT('Ctrl Pts',(-0.928429249625612,0.417746114456447,
-2.15166537899158)) ;
#48904=CARTESIAN_POINT('Ctrl Pts',(-0.974026766105337,0.296362315267558,
-2.13925583836098)) ;
#48905=CARTESIAN_POINT('Ctrl Pts',(-1.01801817035029,0.0380316545170728,
-2.11218534109918)) ;
#48906=CARTESIAN_POINT('Ctrl Pts',(-1.01413682011532,-0.09663341981603,
-2.09807377371727)) ;
#48907=CARTESIAN_POINT('Ctrl Pts',(-0.954440915256791,-0.35585090227032,
-2.07091034631534)) ;
#48908=CARTESIAN_POINT('Ctrl Pts',(-0.899581070501349,-0.477827632577549,
-2.05896864865341)) ;
#48909=CARTESIAN_POINT('Ctrl Pts',(-0.747285042663379,-0.69173530390667,
-2.03393994427587)) ;
#48910=CARTESIAN_POINT('Ctrl Pts',(-0.652104257507281,-0.78208861345665,
-2.02056813653222)) ;
#48911=CARTESIAN_POINT('Ctrl Pts',(-0.428574690228414,-0.924427794215891,
-1.99282475964021)) ;
#48912=CARTESIAN_POINT('Ctrl Pts',(-0.301243647016655,-0.973405364852332,
-1.97870317127512)) ;
#48913=CARTESIAN_POINT('Ctrl Pts',(-0.112364114618148,-1.00527064570199,
-1.95989260184148)) ;
#48914=CARTESIAN_POINT('Ctrl Pts',(-0.0561781570330956,-1.00995540144767,
-1.9545482179547)) ;
#48915=CARTESIAN_POINT('Ctrl Pts',(-1.6057824233506E-13,-1.00995540144768,
-1.94945000000002)) ;
#48916=CARTESIAN_POINT('Ctrl Pts',(-3.96718913291035E-13,-1.00995540144768,
-1.87007500000004)) ;
#48917=CARTESIAN_POINT('Ctrl Pts',(-0.0532324031388302,-1.00995540144766,
-1.8749058881563)) ;
#48918=CARTESIAN_POINT('Ctrl Pts',(-0.106483666306345,-1.00574880487635,
-1.87995889272685)) ;
#48919=CARTESIAN_POINT('Ctrl Pts',(-0.292825540902382,-0.975986710216376,
-1.8984289708955)) ;
#48920=CARTESIAN_POINT('Ctrl Pts',(-0.420680856549743,-0.928062759352234,
-1.91254293298895)) ;
#48921=CARTESIAN_POINT('Ctrl Pts',(-0.645586111849608,-0.787495464559284,
-1.94031831673936)) ;
#48922=CARTESIAN_POINT('Ctrl Pts',(-0.741589518910646,-0.697857228405682,
-1.95372731184761)) ;
#48923=CARTESIAN_POINT('Ctrl Pts',(-0.895493231454798,-0.485360289051763,
-1.9788279996725)) ;
#48924=CARTESIAN_POINT('Ctrl Pts',(-0.951256265240327,-0.364160496663927,
-1.99066458303998)) ;
#48925=CARTESIAN_POINT('Ctrl Pts',(-1.01324774041705,-0.105696196860988,
-2.01774908435222)) ;
#48926=CARTESIAN_POINT('Ctrl Pts',(-1.01832881772648,0.0290466284782181,
-2.03186879927028)) ;
#48927=CARTESIAN_POINT('Ctrl Pts',(-0.976558289733235,0.287951762494217,
-2.05899949564633)) ;
#48928=CARTESIAN_POINT('Ctrl Pts',(-0.931971481044396,0.409800986068976,
-2.07155263290278)) ;
#48929=CARTESIAN_POINT('Ctrl Pts',(-0.796686838022514,0.635098512061202,
-2.09563431094332)) ;
#48930=CARTESIAN_POINT('Ctrl Pts',(-0.705276453944694,0.73525726628461,
-2.10917770821186)) ;
#48931=CARTESIAN_POINT('Ctrl Pts',(-0.490642543662654,0.892570302392133,
-2.13689835222457)) ;
#48932=CARTESIAN_POINT('Ctrl Pts',(-0.369970882133026,0.948970636135906,
-2.15080451181635)) ;
#48933=CARTESIAN_POINT('Ctrl Pts',(-0.116839143478311,1.01140328883631,
-2.17704760545166)) ;
#48934=CARTESIAN_POINT('Ctrl Pts',(0.0128096373669957,1.0180453032631,-2.18831361520504)) ;
#48935=CARTESIAN_POINT('Ctrl Pts',(0.274454571680543,0.981345739588494,
-2.21398100239395)) ;
#48936=CARTESIAN_POINT('Ctrl Pts',(0.403419928429485,0.935729881775167,
-2.22807476905191)) ;
#48937=CARTESIAN_POINT('Ctrl Pts',(0.631266978248035,0.799057813066932,
-2.25591303270715)) ;
#48938=CARTESIAN_POINT('Ctrl Pts',(0.729039556487895,0.710999210621054,
-2.26939981668926)) ;
#48939=CARTESIAN_POINT('Ctrl Pts',(0.886417892194377,0.501575802907125,
-2.29465479181844)) ;
#48940=CARTESIAN_POINT('Ctrl Pts',(0.94412557286881,0.382039945305987,-2.3062909937258)) ;
#48941=CARTESIAN_POINT('Ctrl Pts',(1.0110528108713,0.125229171849372,-2.33320222183732)) ;
#48942=CARTESIAN_POINT('Ctrl Pts',(1.01872908421214,-0.00964540011792789,
-2.34733574249848)) ;
#48943=CARTESIAN_POINT('Ctrl Pts',(0.981804085738894,-0.269517792034247,
-2.3745677979322)) ;
#48944=CARTESIAN_POINT('Ctrl Pts',(0.939486941403989,-0.392406817819474,
-2.38744535194132)) ;
#48945=CARTESIAN_POINT('Ctrl Pts',(0.808252887693214,-0.620249099775226,
-2.41132096876468)) ;
#48946=CARTESIAN_POINT('Ctrl Pts',(0.718772385618642,-0.722113821672774,
-2.42476428887626)) ;
#48947=CARTESIAN_POINT('Ctrl Pts',(0.50667115026837,-0.883605021828442,
-2.45247400550182)) ;
#48948=CARTESIAN_POINT('Ctrl Pts',(0.386817191786182,-0.94226080444667,
-2.46642413217434)) ;
#48949=CARTESIAN_POINT('Ctrl Pts',(0.174328275065335,-0.99865086313136,
-2.48866225136547)) ;
#48950=CARTESIAN_POINT('Ctrl Pts',(0.0872926934494732,-1.00995540144781,
-2.49715311005985)) ;
#48951=CARTESIAN_POINT('Ctrl Pts',(-1.59255949056786E-12,-1.00995540144768,
-2.50507500000015)) ;
#48952=CARTESIAN_POINT('Origin',(1.04083408558609E-16,-6.38378239159465E-15,
-4.1322625)) ;
#48953=CARTESIAN_POINT('',(-1.04524481388633E-12,-1.00995540144768,-3.2194500000002)) ;
#48954=CARTESIAN_POINT('',(-1.02102525789085E-12,-1.00995540144768,-3.14007500000019)) ;
#48955=CARTESIAN_POINT('',(8.448295215077E-17,-1.00995540144768,-4.1322625)) ;
#48956=CARTESIAN_POINT('Ctrl Pts',(-2.0905741107248E-12,-1.00995540144768,
-3.2194500000002)) ;
#48957=CARTESIAN_POINT('Ctrl Pts',(0.0957964344610122,-1.00995540144787,
-3.21075638796364)) ;
#48958=CARTESIAN_POINT('Ctrl Pts',(0.19120672053905,-0.99634144807684,-3.20138451543131)) ;
#48959=CARTESIAN_POINT('Ctrl Pts',(0.410677519689301,-0.932154392330389,
-3.17810426009695)) ;
#48960=CARTESIAN_POINT('Ctrl Pts',(0.529290181800663,-0.870295210259502,
-3.16409893989565)) ;
#48961=CARTESIAN_POINT('Ctrl Pts',(0.738318065068587,-0.702351931339841,
-3.13633007571004)) ;
#48962=CARTESIAN_POINT('Ctrl Pts',(0.825761940824997,-0.597043690489556,
-3.12326427147137)) ;
#48963=CARTESIAN_POINT('Ctrl Pts',(0.950958390039551,-0.363863299157179,
-3.09882927360186)) ;
#48964=CARTESIAN_POINT('Ctrl Pts',(0.9896403084229,-0.239360706883989,-3.08578263378982)) ;
#48965=CARTESIAN_POINT('Ctrl Pts',(1.01858275692398,0.0223233789725686,
-3.05836073075649)) ;
#48966=CARTESIAN_POINT('Ctrl Pts',(1.00661630445378,0.157307122392741,-3.04421577000725)) ;
#48967=CARTESIAN_POINT('Ctrl Pts',(0.931611065810261,0.411311432915673,
-3.01759863144336)) ;
#48968=CARTESIAN_POINT('Ctrl Pts',(0.870707847851678,0.528146027334785,
-3.00621194294102)) ;
#48969=CARTESIAN_POINT('Ctrl Pts',(0.707588663772576,0.732417261249297,
-2.98070592911035)) ;
#48970=CARTESIAN_POINT('Ctrl Pts',(0.606923010414609,0.817763754257943,
-2.96709869709325)) ;
#48971=CARTESIAN_POINT('Ctrl Pts',(0.375590136282912,0.947093381198886,
-2.93932879939114)) ;
#48972=CARTESIAN_POINT('Ctrl Pts',(0.246384826922,0.988624483967684,-2.92542727777577)) ;
#48973=CARTESIAN_POINT('Ctrl Pts',(-0.0148652763260574,1.01798314072302,
-2.90018034906513)) ;
#48974=CARTESIAN_POINT('Ctrl Pts',(-0.144033550107956,1.00785891794961,
-2.88876898124755)) ;
#48975=CARTESIAN_POINT('Ctrl Pts',(-0.395501569538245,0.938665130084104,
-2.86232262158413)) ;
#48976=CARTESIAN_POINT('Ctrl Pts',(-0.514915155885511,0.878844629487194,
-2.84835143361631)) ;
#48977=CARTESIAN_POINT('Ctrl Pts',(-0.725575354948663,0.715278209202896,
-2.82066376105321)) ;
#48978=CARTESIAN_POINT('Ctrl Pts',(-0.814101920087096,0.612561823008408,
-2.80739041821926)) ;
#48979=CARTESIAN_POINT('Ctrl Pts',(-0.943242638055044,0.383332661133499,
-2.78336947010249)) ;
#48980=CARTESIAN_POINT('Ctrl Pts',(-0.984405913632964,0.259916848341857,
-2.77043671402726)) ;
#48981=CARTESIAN_POINT('Ctrl Pts',(-1.01879134190542,-0.00056030937650664,
-2.74314128512119)) ;
#48982=CARTESIAN_POINT('Ctrl Pts',(-1.00974735449863,-0.135484342474438,
-2.72900258142292)) ;
#48983=CARTESIAN_POINT('Ctrl Pts',(-0.940234363958862,-0.391410312108166,
-2.70218407199758)) ;
#48984=CARTESIAN_POINT('Ctrl Pts',(-0.881505880054271,-0.510078366429226,
-2.69063853006172)) ;
#48985=CARTESIAN_POINT('Ctrl Pts',(-0.722297327848802,-0.717869274875705,
-2.66530299603511)) ;
#48986=CARTESIAN_POINT('Ctrl Pts',(-0.623598107285679,-0.805077049722201,
-2.65177669759113)) ;
#48987=CARTESIAN_POINT('Ctrl Pts',(-0.3942196666315,-0.939661430427828,
-2.62390884337232)) ;
#48988=CARTESIAN_POINT('Ctrl Pts',(-0.264682712776882,-0.984044703498763,
-2.60982778510897)) ;
#48989=CARTESIAN_POINT('Ctrl Pts',(-0.0869379197352431,-1.00715194062447,
-2.59248658138664)) ;
#48990=CARTESIAN_POINT('Ctrl Pts',(-0.0434531465249614,-1.00995540144762,
-2.58839341187931)) ;
#48991=CARTESIAN_POINT('Ctrl Pts',(-1.30495226312157E-12,-1.00995540144768,
-2.58445000000013)) ;
#48992=CARTESIAN_POINT('Ctrl Pts',(-1.59255949056786E-12,-1.00995540144768,
-2.50507500000015)) ;
#48993=CARTESIAN_POINT('Ctrl Pts',(-0.0407512997854664,-1.00995540144761,
-2.50877321687317)) ;
#48994=CARTESIAN_POINT('Ctrl Pts',(-0.0815351550368437,-1.00748961985067,
-2.51260358294113)) ;
#48995=CARTESIAN_POINT('Ctrl Pts',(-0.256866013574687,-0.986128640680006,
-2.52963422467212)) ;
#48996=CARTESIAN_POINT('Ctrl Pts',(-0.386850863150314,-0.94273375662927,
-2.54370414317743)) ;
#48997=CARTESIAN_POINT('Ctrl Pts',(-0.617437752611531,-0.809827169270702,
-2.57159375713428)) ;
#48998=CARTESIAN_POINT('Ctrl Pts',(-0.716871073866336,-0.723305240324533,
-2.58515074093984)) ;
#48999=CARTESIAN_POINT('Ctrl Pts',(-0.877535087260389,-0.51681926064045,
-2.61054998755848)) ;
#49000=CARTESIAN_POINT('Ctrl Pts',(-0.937073888388738,-0.398836931707255,
-2.62203083574432)) ;
#49001=CARTESIAN_POINT('Ctrl Pts',(-1.00863620516127,-0.143621265000624,
-2.64877491245081)) ;
#49002=CARTESIAN_POINT('Ctrl Pts',(-1.01876795823122,-0.00866770045745644,
-2.66291671075234)) ;
#49003=CARTESIAN_POINT('Ctrl Pts',(-0.986405822868516,0.252272244201552,
-2.69026063515088)) ;
#49004=CARTESIAN_POINT('Ctrl Pts',(-0.946163613771282,0.376098738647618,
-2.70323642660011)) ;
#49005=CARTESIAN_POINT('Ctrl Pts',(-0.818696660596608,0.606415026005344,
-2.72737129471121)) ;
#49006=CARTESIAN_POINT('Ctrl Pts',(-0.730933873857989,0.709802076579438,
-2.74051554841513)) ;
#49007=CARTESIAN_POINT('Ctrl Pts',(-0.521431255058484,0.875008802219531,
-2.76818411342067)) ;
#49008=CARTESIAN_POINT('Ctrl Pts',(-0.402375462284226,0.93575218806119,
-2.7821711859232)) ;
#49009=CARTESIAN_POINT('Ctrl Pts',(-0.151367539074259,1.00677805587719,
-2.80867178336935)) ;
#49010=CARTESIAN_POINT('Ctrl Pts',(-0.0223214203910232,1.0178403111084,
-2.82013618089321)) ;
#49011=CARTESIAN_POINT('Ctrl Pts',(0.239080785844768,0.990415501805717,
-2.84529558904638)) ;
#49012=CARTESIAN_POINT('Ctrl Pts',(0.368582276889177,0.949841350688537,
-2.85917384988181)) ;
#49013=CARTESIAN_POINT('Ctrl Pts',(0.600940525489778,0.822185057368149,
-2.88694912682977)) ;
#49014=CARTESIAN_POINT('Ctrl Pts',(0.702295931496101,0.737510000342818,
-2.90058377459226)) ;
#49015=CARTESIAN_POINT('Ctrl Pts',(0.866796281121525,0.534492162085355,
-2.92614945869881)) ;
#49016=CARTESIAN_POINT('Ctrl Pts',(0.928465926229044,0.418298181480813,
-2.93749148932227)) ;
#49017=CARTESIAN_POINT('Ctrl Pts',(1.00540024146006,0.164982481451587,-2.96403646831969)) ;
#49018=CARTESIAN_POINT('Ctrl Pts',(1.01839847450756,0.0299925703233738,
-2.97818207538372)) ;
#49019=CARTESIAN_POINT('Ctrl Pts',(0.991383041591425,-0.232089948657272,
-3.00564573026626)) ;
#49020=CARTESIAN_POINT('Ctrl Pts',(0.953582303138476,-0.356963626180555,
-3.01873125614091)) ;
#49021=CARTESIAN_POINT('Ctrl Pts',(0.830184473602272,-0.590795883260668,
-3.04323456309107)) ;
#49022=CARTESIAN_POINT('Ctrl Pts',(0.74380025283825,-0.696468175413241,
-3.05614928256783)) ;
#49023=CARTESIAN_POINT('Ctrl Pts',(0.53638651456345,-0.865955791938646,
-3.08385257730334)) ;
#49024=CARTESIAN_POINT('Ctrl Pts',(0.418185055368803,-0.928825093038498,
-3.09787350571241)) ;
#49025=CARTESIAN_POINT('Ctrl Pts',(0.196555780740535,-0.99556386004186,
-3.12148334167159)) ;
#49026=CARTESIAN_POINT('Ctrl Pts',(0.0984934115873061,-1.00995540144788,
-3.13113663487926)) ;
#49027=CARTESIAN_POINT('Ctrl Pts',(-2.04213499873386E-12,-1.00995540144768,
-3.14007500000019)) ;
#49028=CARTESIAN_POINT('Origin',(0.,0.,-3.85445)) ;
#49029=CARTESIAN_POINT('',(-9.39890130376564E-14,-1.4224,-0.361950000000022)) ;
#49030=CARTESIAN_POINT('',(-3.86032956577361E-14,-1.4224,-0.282575000000003)) ;
#49031=CARTESIAN_POINT('',(-1.7419376071072E-16,-1.4224,-3.85445)) ;
#49032=CARTESIAN_POINT('',(-0.61037374420954,1.28478233657676,4.2165369315862E-15)) ;
#49033=CARTESIAN_POINT('Ctrl Pts',(-1.8627460685039E-13,-1.42240000000001,
-0.361950000000022)) ;
#49034=CARTESIAN_POINT('Ctrl Pts',(0.111298535710606,-1.42240000000002,
-0.354778321478478)) ;
#49035=CARTESIAN_POINT('Ctrl Pts',(0.222425028327351,-1.40934324081798,
-0.347131986267857)) ;
#49036=CARTESIAN_POINT('Ctrl Pts',(0.514567345684877,-1.33940677840386,
-0.325705580050659)) ;
#49037=CARTESIAN_POINT('Ctrl Pts',(0.687411639031778,-1.25946111472812,
-0.311593944576295)) ;
#49038=CARTESIAN_POINT('Ctrl Pts',(0.98610208539558,-1.04103646075053,-0.284221486138232)) ;
#49039=CARTESIAN_POINT('Ctrl Pts',(1.11078307209736,-0.90683609548697,-0.271194917352188)) ;
#49040=CARTESIAN_POINT('Ctrl Pts',(1.30756113063591,-0.591354007382843,
-0.246778560086278)) ;
#49041=CARTESIAN_POINT('Ctrl Pts',(1.3748864251228,-0.411299926504309,-0.233802673102993)) ;
#49042=CARTESIAN_POINT('Ctrl Pts',(1.43399509839727,-0.0393545326910181,
-0.206128164634742)) ;
#49043=CARTESIAN_POINT('Ctrl Pts',(1.42682973307147,0.148502360842787,-0.192150717199191)) ;
#49044=CARTESIAN_POINT('Ctrl Pts',(1.34187381087908,0.505104411187508,-0.165617826548542)) ;
#49045=CARTESIAN_POINT('Ctrl Pts',(1.26710869380764,0.670945919027301,-0.154053821330338)) ;
#49046=CARTESIAN_POINT('Ctrl Pts',(1.0547168948564,0.972856235825795,-0.129136272829856)) ;
#49047=CARTESIAN_POINT('Ctrl Pts',(0.916425588485012,1.10408702592583,-0.11534317911779)) ;
#49048=CARTESIAN_POINT('Ctrl Pts',(0.600759469129882,1.30237482232973,-0.0876260082340457)) ;
#49049=CARTESIAN_POINT('Ctrl Pts',(0.427364010981002,1.36911390156539,-0.0739701740617537)) ;
#49050=CARTESIAN_POINT('Ctrl Pts',(0.104084296066816,1.42588999826873,-0.0510269825442286)) ;
#49051=CARTESIAN_POINT('Ctrl Pts',(-0.0407736404990986,1.42910084743681,
-0.042071980300692)) ;
#49052=CARTESIAN_POINT('Ctrl Pts',(-0.331656935595464,1.39121979999024,
-0.0219192387223242)) ;
#49053=CARTESIAN_POINT('Ctrl Pts',(-0.475640265106083,1.34879144984809,
-0.0110630336517518)) ;
#49054=CARTESIAN_POINT('Ctrl Pts',(-0.610373744210755,1.28478233657617,
9.84542308790637E-14)) ;
#49055=CARTESIAN_POINT('',(-1.7419376071072E-16,-1.42240000000001,-6.43033109173613E-17)) ;
#49056=CARTESIAN_POINT('Origin',(0.,-5.51039363524674E-15,0.)) ;
#49057=CARTESIAN_POINT('',(-1.7419376071072E-16,-1.42240000000001,0.240832122829321)) ;
#49058=CARTESIAN_POINT('',(-1.7419376071072E-16,-1.4224,-3.85445)) ;
#49059=CARTESIAN_POINT('',(2.51958832456576E-16,1.4224,0.240832122829325)) ;
#49060=CARTESIAN_POINT('Origin',(0.,-5.85469173142172E-15,0.240832122829323)) ;
#49061=CARTESIAN_POINT('Origin',(0.,-5.85469173142172E-15,0.240832122829323)) ;
#49062=CARTESIAN_POINT('',(0.491435946297416,1.33480802765296,2.84791806270966E-16)) ;
#49063=CARTESIAN_POINT('Origin',(0.,-5.51039363524674E-15,0.)) ;
#49064=CARTESIAN_POINT('Ctrl Pts',(0.491435946296152,1.33480802765341,1.05343251483037E-13)) ;
#49065=CARTESIAN_POINT('Ctrl Pts',(0.630545413774582,1.28359212890788,-0.010869068609717)) ;
#49066=CARTESIAN_POINT('Ctrl Pts',(0.760787091978431,1.21094929767397,-0.0219638615839183)) ;
#49067=CARTESIAN_POINT('Ctrl Pts',(0.991591616538777,1.03004741261812,-0.0435660583179642)) ;
#49068=CARTESIAN_POINT('Ctrl Pts',(1.09140420456731,0.923638070437862,-0.0539563044444758)) ;
#49069=CARTESIAN_POINT('Ctrl Pts',(1.27528865898732,0.655250544555112,-0.0757898142532674)) ;
#49070=CARTESIAN_POINT('Ctrl Pts',(1.34798998887735,0.488534773976204,-0.0874756864601226)) ;
#49071=CARTESIAN_POINT('Ctrl Pts',(1.4285974262233,0.130728153192531,-0.114098202887478)) ;
#49072=CARTESIAN_POINT('Ctrl Pts',(1.43341466563187,-0.0574392600133656,
-0.128098754465297)) ;
#49073=CARTESIAN_POINT('Ctrl Pts',(1.36966067712458,-0.428014838436086,
-0.155671342145558)) ;
#49074=CARTESIAN_POINT('Ctrl Pts',(1.30050273368294,-0.606469701281969,
-0.168420717677134)) ;
#49075=CARTESIAN_POINT('Ctrl Pts',(1.10056528640145,-0.919249254739077,
-0.192940113900507)) ;
#49076=CARTESIAN_POINT('Ctrl Pts',(0.974236166010392,-1.05218422456176,
-0.206025806787986)) ;
#49077=CARTESIAN_POINT('Ctrl Pts',(0.672712781348542,-1.26740553763213,
-0.233461637702227)) ;
#49078=CARTESIAN_POINT('Ctrl Pts',(0.498736738258435,-1.34541282634434,
-0.247574086907735)) ;
#49079=CARTESIAN_POINT('Ctrl Pts',(0.211118407590415,-1.41064129264867,
-0.268533834981004)) ;
#49080=CARTESIAN_POINT('Ctrl Pts',(0.105619496935363,-1.42240000000001,
-0.275769258371951)) ;
#49081=CARTESIAN_POINT('Ctrl Pts',(-7.629313847346E-14,-1.4224,-0.282575000000003)) ;
#49082=CARTESIAN_POINT('Origin',(0.,0.,-3.85445)) ;
#49083=CARTESIAN_POINT('',(-3.94675305142138E-13,-1.4224,-0.996950000000061)) ;
#49084=CARTESIAN_POINT('',(-3.54056087750793E-13,-1.4224,-0.917575000000045)) ;
#49085=CARTESIAN_POINT('',(-1.7419376071072E-16,-1.4224,-3.85445)) ;
#49086=CARTESIAN_POINT('Ctrl Pts',(-7.89299181569447E-13,-1.4224,-0.996950000000061)) ;
#49087=CARTESIAN_POINT('Ctrl Pts',(0.138490439042576,-1.42240000000008,
-0.988026172738694)) ;
#49088=CARTESIAN_POINT('Ctrl Pts',(0.276447863211548,-1.40218515201483,
-0.978384650568776)) ;
#49089=CARTESIAN_POINT('Ctrl Pts',(0.589172730868239,-1.30815485863121,
-0.954735630741571)) ;
#49090=CARTESIAN_POINT('Ctrl Pts',(0.756323997591869,-1.21916477894938,
-0.940654359677707)) ;
#49091=CARTESIAN_POINT('Ctrl Pts',(1.04118398257388,-0.985806550942943,
-0.913617522064665)) ;
#49092=CARTESIAN_POINT('Ctrl Pts',(1.15779642989958,-0.845761976126516,
-0.901128718461797)) ;
#49093=CARTESIAN_POINT('Ctrl Pts',(1.33634013558368,-0.522535401145264,
-0.877079122109026)) ;
#49094=CARTESIAN_POINT('Ctrl Pts',(1.39378321370383,-0.340844339738977,
-0.863560441944868)) ;
#49095=CARTESIAN_POINT('Ctrl Pts',(1.43408603973681,0.0309190917051568,
-0.83589947234337)) ;
#49096=CARTESIAN_POINT('Ctrl Pts',(1.4178689094259,0.217297970420088,-0.822031996248509)) ;
#49097=CARTESIAN_POINT('Ctrl Pts',(1.31608556407904,0.569086032652425,-0.795857289237174)) ;
#49098=CARTESIAN_POINT('Ctrl Pts',(1.23316536904834,0.731597852345015,-0.784610238875787)) ;
#49099=CARTESIAN_POINT('Ctrl Pts',(1.00496559334499,1.02446254272169,-0.759010599881342)) ;
#49100=CARTESIAN_POINT('Ctrl Pts',(0.85897615547451,1.14961402324307,-0.744947630972062)) ;
#49101=CARTESIAN_POINT('Ctrl Pts',(0.532802075597663,1.33149312522466,-0.717163807294967)) ;
#49102=CARTESIAN_POINT('Ctrl Pts',(0.357114356937224,1.38897378137191,-0.703704703458175)) ;
#49103=CARTESIAN_POINT('Ctrl Pts',(-0.00803848792455285,1.43432846886466,
-0.678488261221506)) ;
#49104=CARTESIAN_POINT('Ctrl Pts',(-0.19404801621122,1.4211685444779,-0.666900428619501)) ;
#49105=CARTESIAN_POINT('Ctrl Pts',(-0.553888915392507,1.32355145238789,
-0.640081983228383)) ;
#49106=CARTESIAN_POINT('Ctrl Pts',(-0.723807732144668,1.23882000565941,
-0.625980812450659)) ;
#49107=CARTESIAN_POINT('Ctrl Pts',(-1.01525839104091,1.01253198536406,-0.598782324005604)) ;
#49108=CARTESIAN_POINT('Ctrl Pts',(-1.13575754288611,0.87525115937958,-0.585910617188293)) ;
#49109=CARTESIAN_POINT('Ctrl Pts',(-1.32260332165737,0.556323100980893,
-0.562006062113505)) ;
#49110=CARTESIAN_POINT('Ctrl Pts',(-1.38468770998822,0.376176269307061,
-0.548689305752013)) ;
#49111=CARTESIAN_POINT('Ctrl Pts',(-1.43446967338425,0.0049378442003703,
-0.521067399122051)) ;
#49112=CARTESIAN_POINT('Ctrl Pts',(-1.42285680566885,-0.18224902394239,
-0.507139804766191)) ;
#49113=CARTESIAN_POINT('Ctrl Pts',(-1.32964842080824,-0.536520346692677,
-0.480780331347271)) ;
#49114=CARTESIAN_POINT('Ctrl Pts',(-1.25091890948545,-0.700718690590934,
-0.469402991695923)) ;
#49115=CARTESIAN_POINT('Ctrl Pts',(-1.03128016295316,-0.997669939516361,
-0.444202965013257)) ;
#49116=CARTESIAN_POINT('Ctrl Pts',(-0.889888612725,-1.12558983710324,-0.430333275789189)) ;
#49117=CARTESIAN_POINT('Ctrl Pts',(-0.569929244260177,-1.31609920673526,
-0.402628839324504)) ;
#49118=CARTESIAN_POINT('Ctrl Pts',(-0.395427283560689,-1.37862152606662,
-0.389058579604145)) ;
#49119=CARTESIAN_POINT('Ctrl Pts',(-0.1429041702682,-1.41702069898609,-0.371358355079311)) ;
#49120=CARTESIAN_POINT('Ctrl Pts',(-0.071429659967184,-1.4224,-0.366552671139539)) ;
#49121=CARTESIAN_POINT('Ctrl Pts',(-1.87803832314602E-13,-1.4224,-0.361950000000022)) ;
#49122=CARTESIAN_POINT('Ctrl Pts',(-7.70323975547614E-14,-1.4224,-0.282575000000003)) ;
#49123=CARTESIAN_POINT('Ctrl Pts',(-0.0766515080990486,-1.4224,-0.287514148307451)) ;
#49124=CARTESIAN_POINT('Ctrl Pts',(-0.153336559359331,-1.41620565310975,
-0.292685902468706)) ;
#49125=CARTESIAN_POINT('Ctrl Pts',(-0.410801712877122,-1.37414531980365,
-0.310840778226794)) ;
#49126=CARTESIAN_POINT('Ctrl Pts',(-0.584784575647485,-1.30959465944419,
-0.324453048253729)) ;
#49127=CARTESIAN_POINT('Ctrl Pts',(-0.902704858683785,-1.1153355597406,
-0.352165592252209)) ;
#49128=CARTESIAN_POINT('Ctrl Pts',(-1.0426166693825,-0.985815050294616,
-0.365999478939528)) ;
#49129=CARTESIAN_POINT('Ctrl Pts',(-1.25877749321241,-0.686471765330182,
-0.391064390191158)) ;
#49130=CARTESIAN_POINT('Ctrl Pts',(-1.33560136498211,-0.521489468493963,
-0.402523700260881)) ;
#49131=CARTESIAN_POINT('Ctrl Pts',(-1.42485964644578,-0.166095250881975,
-0.428966722404629)) ;
#49132=CARTESIAN_POINT('Ctrl Pts',(-1.43434534633753,0.0214255174811284,
-0.442919160526883)) ;
#49133=CARTESIAN_POINT('Ctrl Pts',(-1.38021362042203,0.392280885279827,
-0.470512565869048)) ;
#49134=CARTESIAN_POINT('Ctrl Pts',(-1.31602914390531,0.571717792568198,
-0.48362739773375)) ;
#49135=CARTESIAN_POINT('Ctrl Pts',(-1.12532984702983,0.888661237299554,
-0.507706427342653)) ;
#49136=CARTESIAN_POINT('Ctrl Pts',(-1.0030572463384,1.02465806853115,-0.520644641182039)) ;
#49137=CARTESIAN_POINT('Ctrl Pts',(-0.708527416893833,1.24765681252985,
-0.54791917142539)) ;
#49138=CARTESIAN_POINT('Ctrl Pts',(-0.537358694150998,1.3303814462102,-0.562026223439437)) ;
#49139=CARTESIAN_POINT('Ctrl Pts',(-0.176621872539829,1.42336780874833,
-0.588730124694257)) ;
#49140=CARTESIAN_POINT('Ctrl Pts',(0.00896772525145244,1.43425304753575,
-0.600211886466829)) ;
#49141=CARTESIAN_POINT('Ctrl Pts',(0.37324274971134,1.38475438273334,-0.62552593092722)) ;
#49142=CARTESIAN_POINT('Ctrl Pts',(0.548449899820525,1.3251536036109,-0.639032942272491)) ;
#49143=CARTESIAN_POINT('Ctrl Pts',(0.872818184805203,1.13917930206659,-0.666852758176575)) ;
#49144=CARTESIAN_POINT('Ctrl Pts',(1.0174569118179,1.01210235889192,-0.680900323917004)) ;
#49145=CARTESIAN_POINT('Ctrl Pts',(1.24203209642853,0.716392979516036,-0.70637223646316)) ;
#49146=CARTESIAN_POINT('Ctrl Pts',(1.32287794180158,0.553052690241605,-0.717675246261794)) ;
#49147=CARTESIAN_POINT('Ctrl Pts',(1.42043614557811,0.200033258872139,-0.743941573000593)) ;
#49148=CARTESIAN_POINT('Ctrl Pts',(1.43438716284087,0.0132420522884449,
-0.757839728252355)) ;
#49149=CARTESIAN_POINT('Ctrl Pts',(1.38942345652445,-0.358191594568931,
-0.785476160310195)) ;
#49150=CARTESIAN_POINT('Ctrl Pts',(1.32972765238025,-0.539134749180973,
-0.798939192647401)) ;
#49151=CARTESIAN_POINT('Ctrl Pts',(1.14710471396944,-0.860241339444908,
-0.822831052042039)) ;
#49152=CARTESIAN_POINT('Ctrl Pts',(1.02861183173671,-0.998953723303938,
-0.835541732495152)) ;
#49153=CARTESIAN_POINT('Ctrl Pts',(0.740439034756506,-1.22891366174676,
-0.862665611370588)) ;
#49154=CARTESIAN_POINT('Ctrl Pts',(0.571917163271546,-1.31582532470112,
-0.876757877239372)) ;
#49155=CARTESIAN_POINT('Ctrl Pts',(0.26383719547491,-1.40399825710552,-0.89988968860181)) ;
#49156=CARTESIAN_POINT('Ctrl Pts',(0.132134173369461,-1.42240000000007,
-0.909060747704911)) ;
#49157=CARTESIAN_POINT('Ctrl Pts',(-7.07073288808147E-13,-1.4224,-0.917575000000044)) ;
#49158=CARTESIAN_POINT('Origin',(0.,0.,-3.85445)) ;
#49159=CARTESIAN_POINT('',(-1.60066293321176E-13,-1.4224,-1.63195000000003)) ;
#49160=CARTESIAN_POINT('',(-2.51750103553702E-13,-1.4224,-1.55257500000003)) ;
#49161=CARTESIAN_POINT('',(-1.7419376071072E-16,-1.4224,-3.85445)) ;
#49162=CARTESIAN_POINT('Ctrl Pts',(-3.2012587025676E-13,-1.4224,-1.63195000000003)) ;
#49163=CARTESIAN_POINT('Ctrl Pts',(0.164881985030532,-1.42240000000004,
-1.62132559615605)) ;
#49164=CARTESIAN_POINT('Ctrl Pts',(0.328691648287487,-1.39374152513343,
-1.6097041253823)) ;
#49165=CARTESIAN_POINT('Ctrl Pts',(0.659540634365683,-1.27397920574445,
-1.58392995972348)) ;
#49166=CARTESIAN_POINT('Ctrl Pts',(0.82075061318887,-1.17660021785233,-1.56991943658728)) ;
#49167=CARTESIAN_POINT('Ctrl Pts',(1.09180355217349,-0.929358504128813,
-1.54325577678126)) ;
#49168=CARTESIAN_POINT('Ctrl Pts',(1.20066148032662,-0.783659607315106,
-1.53150800649667)) ;
#49169=CARTESIAN_POINT('Ctrl Pts',(1.36192384265765,-0.451701405943932,
-1.50680873556131)) ;
#49170=CARTESIAN_POINT('Ctrl Pts',(1.40977001143865,-0.267177756656906,
-1.49307929737031)) ;
#49171=CARTESIAN_POINT('Ctrl Pts',(1.43042550283623,0.105327707786318,-1.46536311698019)) ;
#49172=CARTESIAN_POINT('Ctrl Pts',(1.40474881606367,0.289672845219077,-1.45164696092121)) ;
#49173=CARTESIAN_POINT('Ctrl Pts',(1.28519639268473,0.636117224237128,-1.42586984938713)) ;
#49174=CARTESIAN_POINT('Ctrl Pts',(1.19333408738696,0.795190957391867,-1.41467783900172)) ;
#49175=CARTESIAN_POINT('Ctrl Pts',(0.949750264870148,1.07567253057638,-1.3885475886414)) ;
#49176=CARTESIAN_POINT('Ctrl Pts',(0.798252200174296,1.19242237829718,-1.37444222431765)) ;
#49177=CARTESIAN_POINT('Ctrl Pts',(0.464909851826147,1.35656953071848,-1.34685617386845)) ;
#49178=CARTESIAN_POINT('Ctrl Pts',(0.287449888658176,1.40492952543529,-1.33362218327198)) ;
#49179=CARTESIAN_POINT('Ctrl Pts',(-0.0813378461720174,1.43239880238503,
-1.30883690161707)) ;
#49180=CARTESIAN_POINT('Ctrl Pts',(-0.269258227072101,1.40922494832518,
-1.29660982212353)) ;
#49181=CARTESIAN_POINT('Ctrl Pts',(-0.62488010447269,1.29140534928586,-1.26931165400671)) ;
#49182=CARTESIAN_POINT('Ctrl Pts',(-0.789088546257153,1.19814072133656,
-1.25526098465583)) ;
#49183=CARTESIAN_POINT('Ctrl Pts',(-1.06700509992195,0.957745862977114,
-1.22840977745451)) ;
#49184=CARTESIAN_POINT('Ctrl Pts',(-1.17970267483513,0.814880028955586,
-1.21633095453539)) ;
#49185=CARTESIAN_POINT('Ctrl Pts',(-1.34961355640419,0.48724073148818,-1.19195303061668)) ;
#49186=CARTESIAN_POINT('Ctrl Pts',(-1.40227146194422,0.304066594710712,
-1.17832400258265)) ;
#49187=CARTESIAN_POINT('Ctrl Pts',(-1.43273619922414,-0.0681992273537915,
-1.15062565272666)) ;
#49188=CARTESIAN_POINT('Ctrl Pts',(-1.41176366016459,-0.253619377378095,
-1.13682951061175)) ;
#49189=CARTESIAN_POINT('Ctrl Pts',(-1.30107757466342,-0.602763451894885,
-1.11085152887688)) ;
#49190=CARTESIAN_POINT('Ctrl Pts',(-1.21372293416922,-0.763544300903012,
-1.09966895414397)) ;
#49191=CARTESIAN_POINT('Ctrl Pts',(-0.977842841259858,-1.05029117924816,
-1.07380202022439)) ;
#49192=CARTESIAN_POINT('Ctrl Pts',(-0.829056791780556,-1.1712941195999,
-1.05971318326355)) ;
#49193=CARTESIAN_POINT('Ctrl Pts',(-0.499201735540026,-1.3443902776224,
-1.03201891709671)) ;
#49194=CARTESIAN_POINT('Ctrl Pts',(-0.322574355104637,-1.397341407866,-1.018667773973)) ;
#49195=CARTESIAN_POINT('Ctrl Pts',(-0.0938794309099291,-1.42007914263267,
-1.00308559529349)) ;
#49196=CARTESIAN_POINT('Ctrl Pts',(-0.0469146980627795,-1.42239999999998,
-0.999973014905758)) ;
#49197=CARTESIAN_POINT('Ctrl Pts',(-7.89176416523566E-13,-1.4224,-0.996950000000061)) ;
#49198=CARTESIAN_POINT('Ctrl Pts',(-7.07937981740876E-13,-1.4224,-0.917575000000045)) ;
#49199=CARTESIAN_POINT('Ctrl Pts',(-0.05257531648526,-1.42239999999998,
-0.920962764857756)) ;
#49200=CARTESIAN_POINT('Ctrl Pts',(-0.105204870776728,-1.41948537921627,
-0.924462455437981)) ;
#49201=CARTESIAN_POINT('Ctrl Pts',(-0.339486074083204,-1.39335758485412,
-0.940530712199415)) ;
#49202=CARTESIAN_POINT('Ctrl Pts',(-0.515668509642552,-1.33819051813931,
-0.953935622783672)) ;
#49203=CARTESIAN_POINT('Ctrl Pts',(-0.843752765407469,-1.16079183426805,
-0.981675849123684)) ;
#49204=CARTESIAN_POINT('Ctrl Pts',(-0.99118575839903,-1.0377534239264,-0.995753224306534)) ;
#49205=CARTESIAN_POINT('Ctrl Pts',(-1.22331892209086,-0.748006330871561,
-1.0214903346745)) ;
#49206=CARTESIAN_POINT('Ctrl Pts',(-1.30850322480121,-0.586384969788804,
-1.03269516593834)) ;
#49207=CARTESIAN_POINT('Ctrl Pts',(-1.41485427775941,-0.235945092460195,
-1.05876956157291)) ;
#49208=CARTESIAN_POINT('Ctrl Pts',(-1.43351483611111,-0.0500429157401591,
-1.07260156876934)) ;
#49209=CARTESIAN_POINT('Ctrl Pts',(-1.39825729120866,0.322010964809946,
-1.10028414916741)) ;
#49210=CARTESIAN_POINT('Ctrl Pts',(-1.34326309578732,0.504478797596535,
-1.11386062482118)) ;
#49211=CARTESIAN_POINT('Ctrl Pts',(-1.16914223240554,0.829978719281117,
-1.13807936899414)) ;
#49212=CARTESIAN_POINT('Ctrl Pts',(-1.05454617871205,0.971468160551696,
-1.15034808780115)) ;
#49213=CARTESIAN_POINT('Ctrl Pts',(-0.773254992445382,1.20845733692516,
-1.17729004474716)) ;
#49214=CARTESIAN_POINT('Ctrl Pts',(-0.607604626552341,1.29965838567566,
-1.19135685645734)) ;
#49215=CARTESIAN_POINT('Ctrl Pts',(-0.250897438895581,1.4125107507511,-1.21854016514491)) ;
#49216=CARTESIAN_POINT('Ctrl Pts',(-0.0634571043303167,1.43320730400484,
-1.23058399431525)) ;
#49217=CARTESIAN_POINT('Ctrl Pts',(0.304465698032599,1.40136852494623,-1.25547609870566)) ;
#49218=CARTESIAN_POINT('Ctrl Pts',(0.481537650620031,1.35078626936937,-1.26876776068683)) ;
#49219=CARTESIAN_POINT('Ctrl Pts',(0.813222514640509,1.18230167039937,-1.29640837212861)) ;
#49220=CARTESIAN_POINT('Ctrl Pts',(0.963423204148111,1.06348716277857,-1.31050694851179)) ;
#49221=CARTESIAN_POINT('Ctrl Pts',(1.20328783057966,0.779964259574102,-1.33651069193153)) ;
#49222=CARTESIAN_POINT('Ctrl Pts',(1.29296598630153,0.620069637569694,-1.34768886625226)) ;
#49223=CARTESIAN_POINT('Ctrl Pts',(1.40824549883862,0.27231592161513,-1.37356339868935)) ;
#49224=CARTESIAN_POINT('Ctrl Pts',(1.43165952432366,0.0874378248351271,
-1.38731920946167)) ;
#49225=CARTESIAN_POINT('Ctrl Pts',(1.4062762005124,-0.284984689475835,-1.41502921796695)) ;
#49226=CARTESIAN_POINT('Ctrl Pts',(1.35610583426426,-0.468874024874967,
-1.42871146018415)) ;
#49227=CARTESIAN_POINT('Ctrl Pts',(1.19066915502349,-0.798760488338411,
-1.45325658395375)) ;
#49228=CARTESIAN_POINT('Ctrl Pts',(1.07996781480803,-0.943090859244508,
-1.46515430556019)) ;
#49229=CARTESIAN_POINT('Ctrl Pts',(0.805613633508822,-1.18705252303244,
-1.49190865991537)) ;
#49230=CARTESIAN_POINT('Ctrl Pts',(0.642950673153115,-1.28246656113985,
-1.50593970716064)) ;
#49231=CARTESIAN_POINT('Ctrl Pts',(0.316249096520576,-1.3958894711163,-1.53121078750353)) ;
#49232=CARTESIAN_POINT('Ctrl Pts',(0.158587883989674,-1.42240000000006,
-1.54235616545629)) ;
#49233=CARTESIAN_POINT('Ctrl Pts',(-5.03312669319911E-13,-1.4224,-1.55257500000003)) ;
#49234=CARTESIAN_POINT('Origin',(0.,0.,-3.85445)) ;
#49235=CARTESIAN_POINT('',(4.08959556090181E-15,-1.4224,-2.26695000000001)) ;
#49236=CARTESIAN_POINT('',(-1.74193760710719E-16,-1.4224,-2.18757499999999)) ;
#49237=CARTESIAN_POINT('',(-1.7419376071072E-16,-1.4224,-3.85445)) ;
#49238=CARTESIAN_POINT('Ctrl Pts',(8.35338488251435E-15,-1.4224,-2.26695000000001)) ;
#49239=CARTESIAN_POINT('Ctrl Pts',(0.00705824810515262,-1.4224,-2.26649519180319)) ;
#49240=CARTESIAN_POINT('Ctrl Pts',(0.0141185381379087,-1.42234746325677,
-2.26603829753993)) ;
#49241=CARTESIAN_POINT('Ctrl Pts',(0.20238837868152,-1.41954371511923,-2.2538025580499)) ;
#49242=CARTESIAN_POINT('Ctrl Pts',(0.381364936782223,-1.38224015132245,
-2.24088216906958)) ;
#49243=CARTESIAN_POINT('Ctrl Pts',(0.722111878701266,-1.23983456884393,
-2.21362783133127)) ;
#49244=CARTESIAN_POINT('Ctrl Pts',(0.879641651811128,-1.13352368170617,
-2.19952215953555)) ;
#49245=CARTESIAN_POINT('Ctrl Pts',(1.14150362023217,-0.86844369091499,-2.17278710653457)) ;
#49246=CARTESIAN_POINT('Ctrl Pts',(1.24431409242575,-0.713370649668091,
-2.1612781733384)) ;
#49247=CARTESIAN_POINT('Ctrl Pts',(1.38467644681224,-0.373504162954386,
-2.13599048831506)) ;
#49248=CARTESIAN_POINT('Ctrl Pts',(1.42122825231272,-0.192142196309621,
-2.12249629436828)) ;
#49249=CARTESIAN_POINT('Ctrl Pts',(1.42356155502621,0.181630074663026,-2.09468585753996)) ;
#49250=CARTESIAN_POINT('Ctrl Pts',(1.38646443566518,0.370488269493329,-2.08063390851984)) ;
#49251=CARTESIAN_POINT('Ctrl Pts',(1.24381905453741,0.713298253677465,-2.05512721326805)) ;
#49252=CARTESIAN_POINT('Ctrl Pts',(1.14326175388171,0.86535696644464,-2.04384101479274)) ;
#49253=CARTESIAN_POINT('Ctrl Pts',(0.887180203460197,1.12718288664927,-2.01759949037251)) ;
#49254=CARTESIAN_POINT('Ctrl Pts',(0.732792885628689,1.23313983476483,-2.00370947450034)) ;
#49255=CARTESIAN_POINT('Ctrl Pts',(0.389190744486969,1.38106171658738,-1.97606593849329)) ;
#49256=CARTESIAN_POINT('Ctrl Pts',(0.202768612285937,1.42046772056397,-1.96258756763748)) ;
#49257=CARTESIAN_POINT('Ctrl Pts',(-0.166575902046834,1.42411360973044,
-1.93865269585595)) ;
#49258=CARTESIAN_POINT('Ctrl Pts',(-0.346007778185403,1.39147701313561,
-1.92600409082978)) ;
#49259=CARTESIAN_POINT('Ctrl Pts',(-0.689597944522936,1.25813706190102,
-1.89890380897293)) ;
#49260=CARTESIAN_POINT('Ctrl Pts',(-0.849433289927311,1.1562540977711,-1.88481430364497)) ;
#49261=CARTESIAN_POINT('Ctrl Pts',(-1.1188045432412,0.897749618059628,-1.85784000392214)) ;
#49262=CARTESIAN_POINT('Ctrl Pts',(-1.22624127259538,0.744307332093111,
-1.84608000982836)) ;
#49263=CARTESIAN_POINT('Ctrl Pts',(-1.37507900931244,0.407225124304485,
-1.82099948841552)) ;
#49264=CARTESIAN_POINT('Ctrl Pts',(-1.41598013707408,0.227257966918058,
-1.8076090749195)) ;
#49265=CARTESIAN_POINT('Ctrl Pts',(-1.42765124254203,-0.14540752582436,
-1.77988098766189)) ;
#49266=CARTESIAN_POINT('Ctrl Pts',(-1.39547968562878,-0.334652540650194,
-1.76580025739211)) ;
#49267=CARTESIAN_POINT('Ctrl Pts',(-1.26183834351431,-0.681038000747549,
-1.74002752970629)) ;
#49268=CARTESIAN_POINT('Ctrl Pts',(-1.16495811008005,-0.836018033780636,
-1.72883052833213)) ;
#49269=CARTESIAN_POINT('Ctrl Pts',(-0.915543325834338,-1.10419215095865,
-1.7027824183749)) ;
#49270=CARTESIAN_POINT('Ctrl Pts',(-0.764306362432892,-1.21378811464194,
-1.6889600200146)) ;
#49271=CARTESIAN_POINT('Ctrl Pts',(-0.431330658955535,-1.36755835010461,
-1.66178364086345)) ;
#49272=CARTESIAN_POINT('Ctrl Pts',(-0.253175504627166,-1.41145280119291,
-1.64867098348413)) ;
#49273=CARTESIAN_POINT('Ctrl Pts',(-0.0476886137906572,-1.42180093277766,
-1.635045169987)) ;
#49274=CARTESIAN_POINT('Ctrl Pts',(-0.0238345165532617,-1.4224,-1.63348581077546)) ;
#49275=CARTESIAN_POINT('Ctrl Pts',(-3.19958392881641E-13,-1.4224,-1.63195000000003)) ;
#49276=CARTESIAN_POINT('Ctrl Pts',(-5.03326013346693E-13,-1.4224,-1.55257500000003)) ;
#49277=CARTESIAN_POINT('Ctrl Pts',(-0.0292793697530499,-1.42239999999999,
-1.55446165759024)) ;
#49278=CARTESIAN_POINT('Ctrl Pts',(-0.0585860447358915,-1.42149597301951,
-1.5563837065877)) ;
#49279=CARTESIAN_POINT('Ctrl Pts',(-0.269603865804769,-1.40843387270665,
-1.57046687949346)) ;
#49280=CARTESIAN_POINT('Ctrl Pts',(-0.44744011881166,-1.36240077891355,
-1.58363855060316)) ;
#49281=CARTESIAN_POINT('Ctrl Pts',(-0.782456997879084,-1.20280699617351,
-1.6111631056135)) ;
#49282=CARTESIAN_POINT('Ctrl Pts',(-0.935282858313713,-1.08823109080047,
-1.62527315250176)) ;
#49283=CARTESIAN_POINT('Ctrl Pts',(-1.18274523279402,-0.810949888412982,
-1.65153426142843)) ;
#49284=CARTESIAN_POINT('Ctrl Pts',(-1.27689640477158,-0.652732684199964,
-1.66275858004465)) ;
#49285=CARTESIAN_POINT('Ctrl Pts',(-1.40273768552504,-0.302515682358636,
-1.68881639268165)) ;
#49286=CARTESIAN_POINT('Ctrl Pts',(-1.43052151306998,-0.113030283103728,
-1.70291500869764)) ;
#49287=CARTESIAN_POINT('Ctrl Pts',(-1.41056802361381,0.258456000534885,
-1.73055535718265)) ;
#49288=CARTESIAN_POINT('Ctrl Pts',(-1.36582692532895,0.437092117957235,
-1.74384673496706)) ;
#49289=CARTESIAN_POINT('Ctrl Pts',(-1.20941761067431,0.771634853533995,
-1.76873830755461)) ;
#49290=CARTESIAN_POINT('Ctrl Pts',(-1.09776182740402,0.923610562026558,
-1.78078300976017)) ;
#49291=CARTESIAN_POINT('Ctrl Pts',(-0.821656418115741,1.17608484817488,
-1.80796689678696)) ;
#49292=CARTESIAN_POINT('Ctrl Pts',(-0.659843409673311,1.27393039077089,
-1.82203363393517)) ;
#49293=CARTESIAN_POINT('Ctrl Pts',(-0.313952818508723,1.39901801775358,
-1.84897514080793)) ;
#49294=CARTESIAN_POINT('Ctrl Pts',(-0.134120162014341,1.42750475630256,
-1.86124286862981)) ;
#49295=CARTESIAN_POINT('Ctrl Pts',(0.23483026846509,1.41552441729608,-1.88546240843901)) ;
#49296=CARTESIAN_POINT('Ctrl Pts',(0.420346453896695,1.37190502931201,-1.89903915125069)) ;
#49297=CARTESIAN_POINT('Ctrl Pts',(0.760172461443112,1.21639076140491,-1.92672182158963)) ;
#49298=CARTESIAN_POINT('Ctrl Pts',(0.911830410768999,1.10727033778187,-1.94055365556386)) ;
#49299=CARTESIAN_POINT('Ctrl Pts',(1.16212837930198,0.83993220336767,-1.96662757420019)) ;
#49300=CARTESIAN_POINT('Ctrl Pts',(1.25949542454028,0.685342539624457,-1.97783225151605)) ;
#49301=CARTESIAN_POINT('Ctrl Pts',(1.39433503064672,0.339427069423941,-2.00357000971548)) ;
#49302=CARTESIAN_POINT('Ctrl Pts',(1.42716082271295,0.15022630792033,-2.01764744732736)) ;
#49303=CARTESIAN_POINT('Ctrl Pts',(1.41672756002279,-0.222599408791518,
-2.04538745601127)) ;
#49304=CARTESIAN_POINT('Ctrl Pts',(1.37640177539242,-0.402757885947333,
-2.05879210460918)) ;
#49305=CARTESIAN_POINT('Ctrl Pts',(1.22869104674956,-0.740213868060773,
-2.08390043661167)) ;
#49306=CARTESIAN_POINT('Ctrl Pts',(1.12187530325842,-0.893873509519988,
-2.09562293469196)) ;
#49307=CARTESIAN_POINT('Ctrl Pts',(0.853504449015797,-1.15326286123838,
-2.12256569163159)) ;
#49308=CARTESIAN_POINT('Ctrl Pts',(0.693970220958235,-1.255740275215,-2.13665790898719)) ;
#49309=CARTESIAN_POINT('Ctrl Pts',(0.353622076028277,-1.38916742812599,
-2.1635525307205)) ;
#49310=CARTESIAN_POINT('Ctrl Pts',(0.177520453174637,-1.4224,-2.17613621859073)) ;
#49311=CARTESIAN_POINT('Ctrl Pts',(-1.73472347597681E-16,-1.4224,-2.18757499999999)) ;
#49312=CARTESIAN_POINT('Origin',(0.,0.,-3.85445)) ;
#49313=CARTESIAN_POINT('',(2.79104006804924E-13,-1.4224,-2.90194999999997)) ;
#49314=CARTESIAN_POINT('',(1.19211907244443E-13,-1.4224,-2.82257499999998)) ;
#49315=CARTESIAN_POINT('',(-1.7419376071072E-16,-1.4224,-3.85445)) ;
#49316=CARTESIAN_POINT('Ctrl Pts',(5.58382207370559E-13,-1.4224,-2.90194999999997)) ;
#49317=CARTESIAN_POINT('Ctrl Pts',(0.0311347855562209,-1.4224,-2.89994378606897)) ;
#49318=CARTESIAN_POINT('Ctrl Pts',(0.0622995603867949,-1.42137777228308,
-2.89789761043169)) ;
#49319=CARTESIAN_POINT('Ctrl Pts',(0.27519485177764,-1.40736126326523,-2.88365795379482)) ;
#49320=CARTESIAN_POINT('Ctrl Pts',(0.452916575232848,-1.36059958990392,
-2.87046655766408)) ;
#49321=CARTESIAN_POINT('Ctrl Pts',(0.787415833678526,-1.19957881152357,
-2.84292226863498)) ;
#49322=CARTESIAN_POINT('Ctrl Pts',(0.939829311069727,-1.08432089525593,
-2.82881342180211)) ;
#49323=CARTESIAN_POINT('Ctrl Pts',(1.18607923031601,-0.806035459267605,
-2.80259307926183)) ;
#49324=CARTESIAN_POINT('Ctrl Pts',(1.27951302222529,-0.6475510913556,-2.79138088477348)) ;
#49325=CARTESIAN_POINT('Ctrl Pts',(1.40211900625454,-0.302048982793983,
-2.76567388264836)) ;
#49326=CARTESIAN_POINT('Ctrl Pts',(1.4294067606685,-0.118101449897238,-2.75198731026021)) ;
#49327=CARTESIAN_POINT('Ctrl Pts',(1.41212858153763,0.254426175771634,-2.72426948096937)) ;
#49328=CARTESIAN_POINT('Ctrl Pts',(1.36594844361767,0.439384554082642,-2.71050769686885)) ;
#49329=CARTESIAN_POINT('Ctrl Pts',(1.20767557248197,0.772811623871518,-2.68569913512861)) ;
#49330=CARTESIAN_POINT('Ctrl Pts',(1.10012700707919,0.919492133416788,-2.67404760928657)) ;
#49331=CARTESIAN_POINT('Ctrl Pts',(0.831425064010638,1.16905521759255,-2.64744907871875)) ;
#49332=CARTESIAN_POINT('Ctrl Pts',(0.671261647153545,1.26781760859926,-2.63345452639297)) ;
#49333=CARTESIAN_POINT('Ctrl Pts',(0.318759110331852,1.39915779684059,-2.60585435928681)) ;
#49334=CARTESIAN_POINT('Ctrl Pts',(0.129508016637823,1.42913284796985,-2.59304551014784)) ;
#49335=CARTESIAN_POINT('Ctrl Pts',(-0.24154172827379,1.41347133802415,-2.5685537497212)) ;
#49336=CARTESIAN_POINT('Ctrl Pts',(-0.419906890651167,1.37108939873629,
-2.55548382922917)) ;
#49337=CARTESIAN_POINT('Ctrl Pts',(-0.757426125987458,1.21866433628123,
-2.52806472481737)) ;
#49338=CARTESIAN_POINT('Ctrl Pts',(-0.912272533936138,1.10752435050957,
-2.51395230548298)) ;
#49339=CARTESIAN_POINT('Ctrl Pts',(-1.16578521716074,0.835306996806831,
-2.48748972358525)) ;
#49340=CARTESIAN_POINT('Ctrl Pts',(-1.26354262584752,0.678416217719143,
-2.47617739715172)) ;
#49341=CARTESIAN_POINT('Ctrl Pts',(-1.39443401940236,0.335510588952948,
-2.45066358548757)) ;
#49342=CARTESIAN_POINT('Ctrl Pts',(-1.4260680404596,0.152711926799914,-2.43706249455356)) ;
#49343=CARTESIAN_POINT('Ctrl Pts',(-1.41794705565271,-0.21972011849095,
-2.409351776898)) ;
#49344=CARTESIAN_POINT('Ctrl Pts',(-1.37630824974514,-0.4057799169763,-2.39550804189165)) ;
#49345=CARTESIAN_POINT('Ctrl Pts',(-1.22617739199268,-0.743144079566568,
-2.37040654169892)) ;
#49346=CARTESIAN_POINT('Ctrl Pts',(-1.12215176235947,-0.892505719027026,
-2.35897076440412)) ;
#49347=CARTESIAN_POINT('Ctrl Pts',(-0.859797106385966,-1.14827735225385,
-2.33255025744819)) ;
#49348=CARTESIAN_POINT('Ctrl Pts',(-0.702506433381979,-1.25070748494266,
-2.31860436571127)) ;
#49349=CARTESIAN_POINT('Ctrl Pts',(-0.361326586308873,-1.38769425018157,
-2.2915237260205)) ;
#49350=CARTESIAN_POINT('Ctrl Pts',(-0.181419697111433,-1.4224,-2.27864003470577)) ;
#49351=CARTESIAN_POINT('Ctrl Pts',(8.53483950180589E-15,-1.4224,-2.26695000000001)) ;
#49352=CARTESIAN_POINT('Ctrl Pts',(-1.74193760710719E-16,-1.4224,-2.18757499999999)) ;
#49353=CARTESIAN_POINT('Ctrl Pts',(-0.00310549422719388,-1.4224,-2.1877751069116)) ;
#49354=CARTESIAN_POINT('Ctrl Pts',(-0.00621137440850784,-1.4223898297657,
-2.18797561704965)) ;
#49355=CARTESIAN_POINT('Ctrl Pts',(-0.198046631073437,-1.42113316446034,
-2.20038354400397)) ;
#49356=CARTESIAN_POINT('Ctrl Pts',(-0.38459361681943,-1.38234820102978,
-2.21384685578751)) ;
#49357=CARTESIAN_POINT('Ctrl Pts',(-0.728736496056371,-1.23555032030395,
-2.24148341950132)) ;
#49358=CARTESIAN_POINT('Ctrl Pts',(-0.883519623551189,-1.13006407827464,
-2.25538142854168)) ;
#49359=CARTESIAN_POINT('Ctrl Pts',(-1.14044867755491,-0.869051457763149,
-2.28164730636856)) ;
#49360=CARTESIAN_POINT('Ctrl Pts',(-1.24147395732859,-0.717359988743452,
-2.29295000083755)) ;
#49361=CARTESIAN_POINT('Ctrl Pts',(-1.38525721567935,-0.375009004575994,
-2.31842254430239)) ;
#49362=CARTESIAN_POINT('Ctrl Pts',(-1.42297820556566,-0.186208635731148,
-2.33247019079382)) ;
#49363=CARTESIAN_POINT('Ctrl Pts',(-1.42183065443789,0.187687440960692,
-2.3602898393572)) ;
#49364=CARTESIAN_POINT('Ctrl Pts',(-1.3858326469319,0.369218569025883,-2.37379661971919)) ;
#49365=CARTESIAN_POINT('Ctrl Pts',(-1.24654246132111,0.709432919902523,
-2.39911018749276)) ;
#49366=CARTESIAN_POINT('Ctrl Pts',(-1.14431012112672,0.864711810806592,
-2.41059243085566)) ;
#49367=CARTESIAN_POINT('Ctrl Pts',(-0.883395687678344,1.13061080258421,
-2.43729689688759)) ;
#49368=CARTESIAN_POINT('Ctrl Pts',(-0.726164177462196,1.23747476251475,
-2.45140392531674)) ;
#49369=CARTESIAN_POINT('Ctrl Pts',(-0.385770146025108,1.38102462402414,
-2.47867809267357)) ;
#49370=CARTESIAN_POINT('Ctrl Pts',(-0.206855967887497,1.4189067249851,-2.49161598507274)) ;
#49371=CARTESIAN_POINT('Ctrl Pts',(0.162973862078443,1.42556422860031,-2.51569416808132)) ;
#49372=CARTESIAN_POINT('Ctrl Pts',(0.350460948395063,1.39142050641088,-2.52880995767405)) ;
#49373=CARTESIAN_POINT('Ctrl Pts',(0.698688059950283,1.25285283966455,-2.55640351111649)) ;
#49374=CARTESIAN_POINT('Ctrl Pts',(0.856336379803752,1.15086935587789,-2.57035583193125)) ;
#49375=CARTESIAN_POINT('Ctrl Pts',(1.11947324965008,0.895858284599545,-2.59679844722876)) ;
#49376=CARTESIAN_POINT('Ctrl Pts',(1.22393218939323,0.746829584895699,-2.60825732255242)) ;
#49377=CARTESIAN_POINT('Ctrl Pts',(1.37507209273564,0.409948276039682,-2.63332289612801)) ;
#49378=CARTESIAN_POINT('Ctrl Pts',(1.41727387607924,0.224018429535852,-2.64715696208812)) ;
#49379=CARTESIAN_POINT('Ctrl Pts',(1.42652621472551,-0.148437749958214,
-2.67486947544333)) ;
#49380=CARTESIAN_POINT('Ctrl Pts',(1.39542743345201,-0.331383956749282,
-2.688481544401)) ;
#49381=CARTESIAN_POINT('Ctrl Pts',(1.26556040407222,-0.674613745434463,
-2.71401947510674)) ;
#49382=CARTESIAN_POINT('Ctrl Pts',(1.16834235645805,-0.831701235349615,
-2.72531580778757)) ;
#49383=CARTESIAN_POINT('Ctrl Pts',(0.915729788520457,-1.10467757850592,
-2.75174862569883)) ;
#49384=CARTESIAN_POINT('Ctrl Pts',(0.761180000069932,-1.21633214604863,
-2.76586107560351)) ;
#49385=CARTESIAN_POINT('Ctrl Pts',(0.424024460116359,-1.36982869321612,
-2.79329660657153)) ;
#49386=CARTESIAN_POINT('Ctrl Pts',(0.245733458969846,-1.41275541284761,
-2.80638201550567)) ;
#49387=CARTESIAN_POINT('Ctrl Pts',(0.0427587296775013,-1.4219183587854,
-2.81980186259364)) ;
#49388=CARTESIAN_POINT('Ctrl Pts',(0.0213712307611172,-1.4224,-2.82119791452758)) ;
#49389=CARTESIAN_POINT('Ctrl Pts',(2.38598008249596E-13,-1.4224,-2.82257499999998)) ;
#49390=CARTESIAN_POINT('Origin',(0.,0.,-3.85445)) ;
#49391=CARTESIAN_POINT('',(1.22356791609788,-0.725329797192901,-3.35280000000001)) ;
#49392=CARTESIAN_POINT('Ctrl Pts',(2.38351005599213E-13,-1.4224,-2.82257499999998)) ;
#49393=CARTESIAN_POINT('Ctrl Pts',(-0.167743111464536,-1.4224,-2.83338376457127)) ;
#49394=CARTESIAN_POINT('Ctrl Pts',(-0.334344174546972,-1.39273727541033,
-2.84522246362053)) ;
#49395=CARTESIAN_POINT('Ctrl Pts',(-0.667041136862354,-1.27005219390176,
-2.87122443995099)) ;
#49396=CARTESIAN_POINT('Ctrl Pts',(-0.827583327651127,-1.17178747294409,
-2.88522488459988)) ;
#49397=CARTESIAN_POINT('Ctrl Pts',(-1.09713364056572,-0.923060689714675,
-2.91184696869191)) ;
#49398=CARTESIAN_POINT('Ctrl Pts',(-1.20515438702793,-0.776735090525134,
-2.92353221052642)) ;
#49399=CARTESIAN_POINT('Ctrl Pts',(-1.36450765096001,-0.443837430686508,
-2.94830138164536)) ;
#49400=CARTESIAN_POINT('Ctrl Pts',(-1.41129001020065,-0.259034280557108,
-2.96205161602999)) ;
#49401=CARTESIAN_POINT('Ctrl Pts',(-1.42978786909493,0.113488908638944,
-2.98976911522613)) ;
#49402=CARTESIAN_POINT('Ctrl Pts',(-1.4030814297501,0.297581655368469,-3.00346649221493)) ;
#49403=CARTESIAN_POINT('Ctrl Pts',(-1.28157828094376,0.643424989524953,
-3.02919888314919)) ;
#49404=CARTESIAN_POINT('Ctrl Pts',(-1.1887133928311,0.802122054212909,-3.04040275528989)) ;
#49405=CARTESIAN_POINT('Ctrl Pts',(-0.943427049507034,1.08120312372754,
-3.0665906079147)) ;
#49406=CARTESIAN_POINT('Ctrl Pts',(-0.791343058130753,1.19700148514056,
-3.08069832969649)) ;
#49407=CARTESIAN_POINT('Ctrl Pts',(-0.457258970750482,1.35915402133909,
-3.10825797067645)) ;
#49408=CARTESIAN_POINT('Ctrl Pts',(-0.27963028250354,1.40649395990625,-3.12146488479448)) ;
#49409=CARTESIAN_POINT('Ctrl Pts',(0.0895500817499499,1.43195430931873,
-3.1462007291939)) ;
#49410=CARTESIAN_POINT('Ctrl Pts',(0.277693631018515,1.40763447297145,-3.15851789452721)) ;
#49411=CARTESIAN_POINT('Ctrl Pts',(0.632804233215071,1.28752447428894,-3.18586832622339)) ;
#49412=CARTESIAN_POINT('Ctrl Pts',(0.796339709168365,1.19331613655909,-3.19991074032015)) ;
#49413=CARTESIAN_POINT('Ctrl Pts',(1.07269829972026,0.951357858332586,-3.22671972090685)) ;
#49414=CARTESIAN_POINT('Ctrl Pts',(1.18452190253661,0.807853041441442,-3.23871688679754)) ;
#49415=CARTESIAN_POINT('Ctrl Pts',(1.35247988444437,0.479229532151915,-3.26316804076252)) ;
#49416=CARTESIAN_POINT('Ctrl Pts',(1.40405255508825,0.29573873272908,-3.27682063000529)) ;
#49417=CARTESIAN_POINT('Ctrl Pts',(1.42949530553819,-0.0396614275677127,
-3.30177599907499)) ;
#49418=CARTESIAN_POINT('Ctrl Pts',(1.41766650813827,-0.187769019916435,
-3.31279590921999)) ;
#49419=CARTESIAN_POINT('Ctrl Pts',(1.35003538825005,-0.470060262619143,
-3.33379972192108)) ;
#49420=CARTESIAN_POINT('Ctrl Pts',(1.29618339295294,-0.602833840132126,
-3.34356377781289)) ;
#49421=CARTESIAN_POINT('Ctrl Pts',(1.22356791609731,-0.725329797193858,
-3.35280000000008)) ;
#49422=CARTESIAN_POINT('',(1.38082735583561,0.341376000000043,-3.35280000000001)) ;
#49423=CARTESIAN_POINT('Origin',(0.,-7.17168199644958E-16,-3.35280000000001)) ;
#49424=CARTESIAN_POINT('Ctrl Pts',(1.380827355836,0.34137599999849,-3.35280000000012)) ;
#49425=CARTESIAN_POINT('Ctrl Pts',(1.34494946230612,0.486498026315639,-3.34200223018486)) ;
#49426=CARTESIAN_POINT('Ctrl Pts',(1.28644929427591,0.624961242933701,-3.33201079970659)) ;
#49427=CARTESIAN_POINT('Ctrl Pts',(1.12759436205324,0.880124714487233,-3.31228206885852)) ;
#49428=CARTESIAN_POINT('Ctrl Pts',(1.02773415600914,0.994900755466381,-3.30157749328181)) ;
#49429=CARTESIAN_POINT('Ctrl Pts',(0.767920662584799,1.21186660616474,-3.27676439723266)) ;
#49430=CARTESIAN_POINT('Ctrl Pts',(0.601792899437461,1.30237154390797,-3.26269272074225)) ;
#49431=CARTESIAN_POINT('Ctrl Pts',(0.244729405122114,1.413560632934,-3.23554833076054)) ;
#49432=CARTESIAN_POINT('Ctrl Pts',(0.0574484938757501,1.43343002083784,
-3.22356211797056)) ;
#49433=CARTESIAN_POINT('Ctrl Pts',(-0.310180545827058,1.40012415083315,
-3.19863436331626)) ;
#49434=CARTESIAN_POINT('Ctrl Pts',(-0.487115735949317,1.34879474425875,
-3.18532371802188)) ;
#49435=CARTESIAN_POINT('Ctrl Pts',(-0.818230503166939,1.17885429923585,
-3.15766568063422)) ;
#49436=CARTESIAN_POINT('Ctrl Pts',(-0.967988546990518,1.05934816381014,
-3.14356989655051)) ;
#49437=CARTESIAN_POINT('Ctrl Pts',(-1.20659871424787,0.774806463283478,
-3.11760908429534)) ;
#49438=CARTESIAN_POINT('Ctrl Pts',(-1.2955435602896,0.61463362657052,-3.10643166864363)) ;
#49439=CARTESIAN_POINT('Ctrl Pts',(-1.40937870005715,0.266440799543008,
-3.08052446425171)) ;
#49440=CARTESIAN_POINT('Ctrl Pts',(-1.43202599105278,0.0813887985564382,
-3.0667557141783)) ;
#49441=CARTESIAN_POINT('Ctrl Pts',(-1.40504464208628,-0.290991981533069,
-3.03904881089783)) ;
#49442=CARTESIAN_POINT('Ctrl Pts',(-1.35409081262042,-0.474660131470722,
-3.02538302593224)) ;
#49443=CARTESIAN_POINT('Ctrl Pts',(-1.18724577345861,-0.803842203239017,
-3.000890312259)) ;
#49444=CARTESIAN_POINT('Ctrl Pts',(-1.0759183915845,-0.947711345213575,
-2.98893787104943)) ;
#49445=CARTESIAN_POINT('Ctrl Pts',(-0.8004455509441,-1.19055603339596,-2.96215298844984)) ;
#49446=CARTESIAN_POINT('Ctrl Pts',(-0.637294720828622,-1.28529834410964,
-2.94811549448515)) ;
#49447=CARTESIAN_POINT('Ctrl Pts',(-0.31202552629567,-1.39659904097479,
-2.92301566308883)) ;
#49448=CARTESIAN_POINT('Ctrl Pts',(-0.156452602692893,-1.4224,-2.91203124467417)) ;
#49449=CARTESIAN_POINT('Ctrl Pts',(5.58382207370559E-13,-1.4224,-2.90194999999997)) ;
#49450=CARTESIAN_POINT('Origin',(1.04083408558609E-16,-6.38378239159465E-15,
-4.1322625)) ;
#49451=CARTESIAN_POINT('',(0.105153794786494,-1.00446632216085,-3.76524459855233)) ;
#49452=CARTESIAN_POINT('Ctrl Pts',(-2.04213499873386E-12,-1.00995540144768,
-3.14007500000019)) ;
#49453=CARTESIAN_POINT('Ctrl Pts',(-0.0294481807784787,-1.00995540144762,
-3.14274744872219)) ;
#49454=CARTESIAN_POINT('Ctrl Pts',(-0.0589227263234698,-1.00866757816801,
-3.14548976563933)) ;
#49455=CARTESIAN_POINT('Ctrl Pts',(-0.22224974390044,-0.994325948900357,
-3.16106326886646)) ;
#49456=CARTESIAN_POINT('Ctrl Pts',(-0.352403824776246,-0.955958878606333,
-3.17488511269584)) ;
#49457=CARTESIAN_POINT('Ctrl Pts',(-0.58707145263758,-0.83217887860383,
-3.20266686928213)) ;
#49458=CARTESIAN_POINT('Ctrl Pts',(-0.689994926562969,-0.749067644977869,
-3.21636188399988)) ;
#49459=CARTESIAN_POINT('Ctrl Pts',(-0.85765553496316,-0.548938105493903,
-3.24206303184746)) ;
#49460=CARTESIAN_POINT('Ctrl Pts',(-0.921076654143625,-0.434195982679694,
-3.25332555705325)) ;
#49461=CARTESIAN_POINT('Ctrl Pts',(-1.00240386668299,-0.182474912493191,
-3.2797034346208)) ;
#49462=CARTESIAN_POINT('Ctrl Pts',(-1.01776124772871,-0.0475000472824059,
-3.29384746502155)) ;
#49463=CARTESIAN_POINT('Ctrl Pts',(-0.995162373102043,0.215439381887664,
-3.32140091561347)) ;
#49464=CARTESIAN_POINT('Ctrl Pts',(-0.959386467255263,0.341136886974746,
-3.33457277046565)) ;
#49465=CARTESIAN_POINT('Ctrl Pts',(-0.840090695756902,0.576437934152737,
-3.35922999208551)) ;
#49466=CARTESIAN_POINT('Ctrl Pts',(-0.756097394197089,0.68293213094862,
-3.37182408423458)) ;
#49467=CARTESIAN_POINT('Ctrl Pts',(-0.552359595968076,0.855892906106022,
-3.39937576045609)) ;
#49468=CARTESIAN_POINT('Ctrl Pts',(-0.435123051699683,0.921045071508901,
-3.41342873276919)) ;
#49469=CARTESIAN_POINT('Ctrl Pts',(-0.186382082707184,1.0008786337726,-3.44018508171057)) ;
#49470=CARTESIAN_POINT('Ctrl Pts',(-0.0578768782872739,1.01642197753821,
-3.4519838049772)) ;
#49471=CARTESIAN_POINT('Ctrl Pts',(0.204166864423636,0.998193749791793,
-3.47671957776183)) ;
#49472=CARTESIAN_POINT('Ctrl Pts',(0.334976010765058,0.962200820461377,
-3.49047647612628)) ;
#49473=CARTESIAN_POINT('Ctrl Pts',(0.572042398711904,0.842616738883757,
-3.51825607696624)) ;
#49474=CARTESIAN_POINT('Ctrl Pts',(0.676617624943253,0.76121127136032,-3.53201161597671)) ;
#49475=CARTESIAN_POINT('Ctrl Pts',(0.847640811743635,0.564186360355263,
-3.55785525364576)) ;
#49476=CARTESIAN_POINT('Ctrl Pts',(0.912923698230532,0.450967386047363,
-3.56906807992056)) ;
#49477=CARTESIAN_POINT('Ctrl Pts',(0.99889282399385,0.200971487538376,-3.59526517656557)) ;
#49478=CARTESIAN_POINT('Ctrl Pts',(1.0167565119974,0.0660569363633425,-3.60940288665213)) ;
#49479=CARTESIAN_POINT('Ctrl Pts',(0.998865597141553,-0.197710566395658,
-3.63704311116301)) ;
#49480=CARTESIAN_POINT('Ctrl Pts',(0.965256077089535,-0.324245770666553,
-3.65030274860126)) ;
#49481=CARTESIAN_POINT('Ctrl Pts',(0.85030427513232,-0.561075523321808,
-3.67512016342977)) ;
#49482=CARTESIAN_POINT('Ctrl Pts',(0.768804038865719,-0.668429348081556,
-3.68741107080029)) ;
#49483=CARTESIAN_POINT('Ctrl Pts',(0.589722281275919,-0.826643482906197,
-3.71195253829972)) ;
#49484=CARTESIAN_POINT('Ctrl Pts',(0.500332228866758,-0.883615481910104,
-3.72304981634036)) ;
#49485=CARTESIAN_POINT('Ctrl Pts',(0.308892965347628,-0.967113466557388,
-3.7447979819066)) ;
#49486=CARTESIAN_POINT('Ctrl Pts',(0.208180352251547,-0.993680860028146,
-3.7553297415333)) ;
#49487=CARTESIAN_POINT('Ctrl Pts',(0.105153794786493,-1.00446632216085,
-3.76524459855233)) ;
#49488=CARTESIAN_POINT('',(0.774268453261688,-0.648473804557356,-3.76524459855233)) ;
#49489=CARTESIAN_POINT('Origin',(-1.52655665885959E-15,-8.32667268468867E-16,
-3.76524459855233)) ;
#49490=CARTESIAN_POINT('Ctrl Pts',(0.774268453261685,-0.648473804557355,
-3.76524459855232)) ;
#49491=CARTESIAN_POINT('Ctrl Pts',(0.840370767588072,-0.569548586127837,
-3.7551104634612)) ;
#49492=CARTESIAN_POINT('Ctrl Pts',(0.893970558333253,-0.481062795668105,
-3.74611062123658)) ;
#49493=CARTESIAN_POINT('Ctrl Pts',(0.974045968545029,-0.287421080478679,
-3.72581888542181)) ;
#49494=CARTESIAN_POINT('Ctrl Pts',(0.998915511899947,-0.183104863629178,
-3.71488757802538)) ;
#49495=CARTESIAN_POINT('Ctrl Pts',(1.01727115688353,0.0573323294145966,
-3.68969213913704)) ;
#49496=CARTESIAN_POINT('Ctrl Pts',(1.00058656044149,0.19228093719233,-3.67555086025547)) ;
#49497=CARTESIAN_POINT('Ctrl Pts',(0.916798193787988,0.44309246430084,-3.64926829380326)) ;
#49498=CARTESIAN_POINT('Ctrl Pts',(0.852391509108282,0.557025563477903,
-3.63803657400815)) ;
#49499=CARTESIAN_POINT('Ctrl Pts',(0.682951053349339,0.755515849489765,
-3.61225979219456)) ;
#49500=CARTESIAN_POINT('Ctrl Pts',(0.579151050689367,0.837729557186524,
-3.59853225762935)) ;
#49501=CARTESIAN_POINT('Ctrl Pts',(0.343206047134314,0.959297696220488,
-3.57075046862974)) ;
#49502=CARTESIAN_POINT('Ctrl Pts',(0.212700111861635,0.996411341438793,
-3.55696236697253)) ;
#49503=CARTESIAN_POINT('Ctrl Pts',(-0.0491996360435293,1.01688069028333,
-3.53212223818676)) ;
#49504=CARTESIAN_POINT('Ctrl Pts',(-0.177830599393395,1.00243281614573,
-3.52041756793102)) ;
#49505=CARTESIAN_POINT('Ctrl Pts',(-0.427136245527989,0.924760364510814,
-3.49372320554004)) ;
#49506=CARTESIAN_POINT('Ctrl Pts',(-0.544834254403358,0.860685319992209,
-3.47968479070716)) ;
#49507=CARTESIAN_POINT('Ctrl Pts',(-0.750311381920156,0.689360432784342,
-3.45206098123404)) ;
#49508=CARTESIAN_POINT('Ctrl Pts',(-0.835432159454808,0.583253987341258,
-3.43931924702003)) ;
#49509=CARTESIAN_POINT('Ctrl Pts',(-0.956669977026895,0.348645229828716,
-3.41473457050743)) ;
#49510=CARTESIAN_POINT('Ctrl Pts',(-0.993407093942808,0.223333825066968,
-3.40160317514917)) ;
#49511=CARTESIAN_POINT('Ctrl Pts',(-1.0181005821026,-0.0392089297094878,
-3.37409129210891)) ;
#49512=CARTESIAN_POINT('Ctrl Pts',(-1.00386109065737,-0.174195975373168,
-3.35994598531722)) ;
#49513=CARTESIAN_POINT('Ctrl Pts',(-0.924612462163221,-0.426676173258984,
-3.33348855867777)) ;
#49514=CARTESIAN_POINT('Ctrl Pts',(-0.862021228541091,-0.542104042455757,
-3.32219229353536)) ;
#49515=CARTESIAN_POINT('Ctrl Pts',(-0.695858586016805,-0.743606186778871,
-3.29655516972656)) ;
#49516=CARTESIAN_POINT('Ctrl Pts',(-0.59367656343571,-0.827463437935267,
-3.28288835475294)) ;
#49517=CARTESIAN_POINT('Ctrl Pts',(-0.360097102063987,-0.95308900066841,
-3.25510865189117)) ;
#49518=CARTESIAN_POINT('Ctrl Pts',(-0.230247952113534,-0.992505220312161,
-3.24125951058011)) ;
#49519=CARTESIAN_POINT('Ctrl Pts',(-0.0643298621211295,-1.0084204317768,
-3.22536841729334)) ;
#49520=CARTESIAN_POINT('Ctrl Pts',(-0.0321504521144425,-1.00995540144761,
-3.22236768226083)) ;
#49521=CARTESIAN_POINT('Ctrl Pts',(-2.0905741107248E-12,-1.00995540144768,
-3.2194500000002)) ;
#49522=CARTESIAN_POINT('Origin',(0.,-1.99494625052956E-16,1.6393)) ;
#49523=CARTESIAN_POINT('',(-2.55525626680218,-5.21339033092948E-16,1.7018)) ;
#49524=CARTESIAN_POINT('Origin',(0.,-2.08410392278897E-16,1.7018)) ;
#49525=CARTESIAN_POINT('',(-2.60242561556611,-5.12350575476211E-16,1.59829631068809)) ;
#49526=CARTESIAN_POINT('Origin',(-2.55525626680218,-5.12423265867006E-16,
1.6393)) ;
#49527=CARTESIAN_POINT('',(-3.18705220012211E-16,2.60242561556611,1.59829631068809)) ;
#49528=CARTESIAN_POINT('Origin',(-3.18705220012211E-16,-2.77555756156289E-16,
1.59829631068809)) ;
#49529=CARTESIAN_POINT('Origin',(-3.18705220012211E-16,-2.77555756156289E-16,
1.59829631068809)) ;
#49530=CARTESIAN_POINT('Origin',(0.,2.40741243048404E-32,0.240832122829324)) ;
#49531=CARTESIAN_POINT('',(-1.7419376071072E-16,1.4224,0.240832122829324)) ;
#49532=CARTESIAN_POINT('Origin',(0.,-2.08410392278897E-16,1.7018)) ;
#49533=CARTESIAN_POINT('',(1.75503707368249,-0.355600000000007,1.7018)) ;
#49534=CARTESIAN_POINT('',(1.75503707368249,0.355600000000001,1.7018)) ;
#49535=CARTESIAN_POINT('Origin',(0.,-1.33894542197505E-16,1.7018)) ;
#49536=CARTESIAN_POINT('',(1.05531853684124,-0.355600000000004,1.7018)) ;
#49537=CARTESIAN_POINT('',(-1.13137151332636E-15,-0.355600000000001,1.7018)) ;
#49538=CARTESIAN_POINT('',(0.56054281451887,-0.560542814518875,1.7018)) ;
#49539=CARTESIAN_POINT('',(0.280271407259434,-0.676635032551125,1.7018)) ;
#49540=CARTESIAN_POINT('',(0.355599999999997,-1.05531853684125,1.7018)) ;
#49541=CARTESIAN_POINT('',(0.676635032551123,-0.280271407259438,1.7018)) ;
#49542=CARTESIAN_POINT('',(0.355599999999995,-1.75503707368249,1.7018)) ;
#49543=CARTESIAN_POINT('',(0.355600000000001,-1.18647113870949E-15,1.7018)) ;
#49544=CARTESIAN_POINT('',(-0.3556,-1.75503707368249,1.7018)) ;
#49545=CARTESIAN_POINT('Origin',(-1.33894542197505E-16,4.67490295455533E-31,
1.7018)) ;
#49546=CARTESIAN_POINT('',(-0.355600000000001,-1.05531853684125,1.7018)) ;
#49547=CARTESIAN_POINT('',(-0.355600000000001,-1.10199250766261E-16,1.7018)) ;
#49548=CARTESIAN_POINT('',(-0.560542814518873,-0.560542814518872,1.7018)) ;
#49549=CARTESIAN_POINT('',(-0.676635032551124,-0.280271407259437,1.7018)) ;
#49550=CARTESIAN_POINT('',(-1.05531853684125,-0.355600000000001,1.7018)) ;
#49551=CARTESIAN_POINT('',(-0.280271407259436,-0.676635032551124,1.7018)) ;
#49552=CARTESIAN_POINT('',(-1.75503707368249,-0.355600000000001,1.7018)) ;
#49553=CARTESIAN_POINT('',(5.50996253831303E-17,-0.355600000000001,1.7018)) ;
#49554=CARTESIAN_POINT('',(-1.75503707368249,0.355600000000019,1.7018)) ;
#49555=CARTESIAN_POINT('Origin',(0.,1.33894542197505E-16,1.7018)) ;
#49556=CARTESIAN_POINT('',(-1.05531853684124,0.355600000000012,1.7018)) ;
#49557=CARTESIAN_POINT('',(3.6145130415116E-15,0.355600000000001,1.7018)) ;
#49558=CARTESIAN_POINT('',(-0.560542814518866,0.560542814518879,1.7018)) ;
#49559=CARTESIAN_POINT('',(-0.28027140725943,0.676635032551127,1.7018)) ;
#49560=CARTESIAN_POINT('',(-0.35559999999999,1.05531853684125,1.7018)) ;
#49561=CARTESIAN_POINT('',(-0.676635032551121,0.280271407259443,1.7018)) ;
#49562=CARTESIAN_POINT('',(-0.355599999999983,1.75503707368249,1.7018)) ;
#49563=CARTESIAN_POINT('',(-0.355600000000001,3.66961266689473E-15,1.7018)) ;
#49564=CARTESIAN_POINT('',(0.3556,1.75503707368249,1.7018)) ;
#49565=CARTESIAN_POINT('Origin',(0.,-1.33894542197505E-16,1.7018)) ;
#49566=CARTESIAN_POINT('',(0.355600000000001,1.05531853684125,1.7018)) ;
#49567=CARTESIAN_POINT('',(0.355600000000001,1.10199250766261E-16,1.7018)) ;
#49568=CARTESIAN_POINT('',(0.560542814518873,0.560542814518872,1.7018)) ;
#49569=CARTESIAN_POINT('',(0.676635032551124,0.280271407259437,1.7018)) ;
#49570=CARTESIAN_POINT('',(1.05531853684125,0.355600000000001,1.7018)) ;
#49571=CARTESIAN_POINT('',(0.280271407259436,0.676635032551124,1.7018)) ;
#49572=CARTESIAN_POINT('',(-5.50996253831303E-17,0.355600000000001,1.7018)) ;
#49573=CARTESIAN_POINT('Origin',(0.,1.88183760310947E-30,-3.85445)) ;
#49574=CARTESIAN_POINT('',(5.12045573059185E-15,1.15468837738307,-3.62051162261693)) ;
#49575=CARTESIAN_POINT('Ctrl Pts',(1.03838891449855E-14,1.15468837738307,
-3.62051162261693)) ;
#49576=CARTESIAN_POINT('Ctrl Pts',(-0.0254296726502328,1.1559680560723,
-3.6192319439277)) ;
#49577=CARTESIAN_POINT('Ctrl Pts',(-0.0508514616237012,1.15642735309998,
-3.61793251315105)) ;
#49578=CARTESIAN_POINT('Ctrl Pts',(-0.233510489525033,1.15388205746895,
-3.60845534611773)) ;
#49579=CARTESIAN_POINT('Ctrl Pts',(-0.388772346045262,1.12045269968389,
-3.59965551646851)) ;
#49580=CARTESIAN_POINT('Ctrl Pts',(-0.668629325046152,0.998730134850622,
-3.58242290709769)) ;
#49581=CARTESIAN_POINT('Ctrl Pts',(-0.792053279372469,0.914879512409016,
-3.57414824333137)) ;
#49582=CARTESIAN_POINT('Ctrl Pts',(-1.03279540943537,0.675197560377038,
-3.55623042073669)) ;
#49583=CARTESIAN_POINT('Ctrl Pts',(-1.11355473457586,0.529659861818994,
-3.54881034220498)) ;
#49584=CARTESIAN_POINT('Ctrl Pts',(-1.22297818921426,0.264095836621968,
-3.53409227811305)) ;
#49585=CARTESIAN_POINT('Ctrl Pts',(-1.2550263520995,0.107380842554988,-3.52557676781509)) ;
#49586=CARTESIAN_POINT('Ctrl Pts',(-1.25910520773258,-0.217034008792059,
-3.50831229920614)) ;
#49587=CARTESIAN_POINT('Ctrl Pts',(-1.22823973733675,-0.381711211853662,
-3.49973959429333)) ;
#49588=CARTESIAN_POINT('Ctrl Pts',(-1.13475227202362,-0.613697014078021,
-3.4878698745816)) ;
#49589=CARTESIAN_POINT('Ctrl Pts',(-1.09529703778593,-0.688397717616974,
-3.48416949380928)) ;
#49590=CARTESIAN_POINT('Ctrl Pts',(-0.960513035812505,-0.89515457262902,
-3.47251753328569)) ;
#49591=CARTESIAN_POINT('Ctrl Pts',(-0.845988378373653,-1.01478305680017,
-3.46424837249028)) ;
#49592=CARTESIAN_POINT('Ctrl Pts',(-0.56869741157037,-1.2132712153186,-3.4469467685559)) ;
#49593=CARTESIAN_POINT('Ctrl Pts',(-0.405690771199438,-1.28628105760199,
-3.43807887608712)) ;
#49594=CARTESIAN_POINT('Ctrl Pts',(-0.00488190160641552,-1.37632292771543,
-3.41885139468694)) ;
#49595=CARTESIAN_POINT('Ctrl Pts',(0.185605942854219,-1.35631716810315,
-3.4111058346593)) ;
#49596=CARTESIAN_POINT('Ctrl Pts',(0.473218634669871,-1.30588042490048,
-3.39746749290741)) ;
#49597=CARTESIAN_POINT('Ctrl Pts',(0.639723227604972,-1.24247603160398,
-3.38887866863048)) ;
#49598=CARTESIAN_POINT('Ctrl Pts',(0.873435804281771,-1.09786424296003,
-3.37571354842859)) ;
#49599=CARTESIAN_POINT('Ctrl Pts',(0.951273721808984,-1.03743011170928,
-3.37108278809331)) ;
#49600=CARTESIAN_POINT('Ctrl Pts',(1.09831291486203,-0.89591089855239,-3.36177284448109)) ;
#49601=CARTESIAN_POINT('Ctrl Pts',(1.16590959394519,-0.814068072356269,
-3.35714783320766)) ;
#49602=CARTESIAN_POINT('Ctrl Pts',(1.22356791609788,-0.7253297971929,-3.3528)) ;
#49603=CARTESIAN_POINT('',(-1.12759354031493E-16,0.92075,-3.85445)) ;
#49604=CARTESIAN_POINT('',(-1.12759354031493E-16,0.92075,-3.85445)) ;
#49605=CARTESIAN_POINT('Origin',(0.,1.88183760310947E-30,-3.85445)) ;
#49606=CARTESIAN_POINT('Ctrl Pts',(0.774268453261687,-0.648473804557357,
-3.76524459855232)) ;
#49607=CARTESIAN_POINT('Ctrl Pts',(0.859102969586174,-0.55913383481557,
-3.75757093331012)) ;
#49608=CARTESIAN_POINT('Ctrl Pts',(0.916121144663882,-0.465482527176917,
-3.75163840738811)) ;
#49609=CARTESIAN_POINT('Ctrl Pts',(0.998843870248869,-0.290638199560699,
-3.73995486333014)) ;
#49610=CARTESIAN_POINT('Ctrl Pts',(1.02887334963585,-0.192294498521731,
-3.73350006306968)) ;
#49611=CARTESIAN_POINT('Ctrl Pts',(1.06402398082417,0.0390726262195363,
-3.71860738004544)) ;
#49612=CARTESIAN_POINT('Ctrl Pts',(1.0591688619149,0.171888637195841,-3.71026675792788)) ;
#49613=CARTESIAN_POINT('Ctrl Pts',(0.99249334900811,0.464810257053766,-3.69226247684784)) ;
#49614=CARTESIAN_POINT('Ctrl Pts',(0.921867648435038,0.593606465432917,
-3.68488414547832)) ;
#49615=CARTESIAN_POINT('Ctrl Pts',(0.768670465162765,0.807762346300646,
-3.66988824166624)) ;
#49616=CARTESIAN_POINT('Ctrl Pts',(0.660201212740624,0.909449744418889,
-3.66103765914579)) ;
#49617=CARTESIAN_POINT('Ctrl Pts',(0.418335514202568,1.05987871318753,-3.64405552581747)) ;
#49618=CARTESIAN_POINT('Ctrl Pts',(0.289099677970515,1.11038390089825,-3.63605666514225)) ;
#49619=CARTESIAN_POINT('Ctrl Pts',(0.10284383143768,1.14596277031152,-3.62580411226576)) ;
#49620=CARTESIAN_POINT('Ctrl Pts',(0.0514158133764808,1.15210101727144,
-3.62309898272856)) ;
#49621=CARTESIAN_POINT('Ctrl Pts',(1.0399667238481E-14,1.15468837738307,
-3.62051162261693)) ;
#49622=CARTESIAN_POINT('Ctrl Pts',(0.105153794786499,-1.00446632216084,
-3.76524459855233)) ;
#49623=CARTESIAN_POINT('Ctrl Pts',(0.195392726897351,-1.01520050247604,
-3.74517332734323)) ;
#49624=CARTESIAN_POINT('Ctrl Pts',(0.286522180585977,-1.01456179720496,
-3.72467512354645)) ;
#49625=CARTESIAN_POINT('Ctrl Pts',(0.46774836542941,-0.990396472641326,
-3.68358102451341)) ;
#49626=CARTESIAN_POINT('Ctrl Pts',(0.557102511311268,-0.966654412138457,
-3.66314099600361)) ;
#49627=CARTESIAN_POINT('Ctrl Pts',(0.766470858342022,-0.881427413527447,
-3.61446326325569)) ;
#49628=CARTESIAN_POINT('Ctrl Pts',(0.880404660110909,-0.80843917966244,
-3.58726411136041)) ;
#49629=CARTESIAN_POINT('Ctrl Pts',(1.00638639259649,-0.690563563660173,
-3.55523972623751)) ;
#49630=CARTESIAN_POINT('Ctrl Pts',(1.06917436077557,-0.62930339582118,-3.54012168635209)) ;
#49631=CARTESIAN_POINT('Ctrl Pts',(1.22604009876658,-0.407710720418697,
-3.49187907348018)) ;
#49632=CARTESIAN_POINT('Ctrl Pts',(1.29218005609473,-0.26941590119793,-3.46374626079454)) ;
#49633=CARTESIAN_POINT('Ctrl Pts',(1.37633487012138,0.0277330507548143,
-3.40722015539582)) ;
#49634=CARTESIAN_POINT('Ctrl Pts',(1.39229240585019,0.184820732040757,-3.37924330459697)) ;
#49635=CARTESIAN_POINT('Ctrl Pts',(1.38082735583561,0.341376000000042,-3.35280000000001)) ;
#49636=CARTESIAN_POINT('Origin',(0.,-5.62590548091936E-17,0.635211073789819)) ;
#49637=CARTESIAN_POINT('',(0.,-5.7099106829244E-18,-0.479172560746747)) ;
#49638=CARTESIAN_POINT('',(-2.19297502323318E-16,1.79070000000001,1.58079214606392)) ;
#49639=CARTESIAN_POINT('',(-1.18633851772253E-16,0.968718914342085,0.635211073789819)) ;
#49640=CARTESIAN_POINT('',(-0.345013184582974,1.75714893861161,1.58079214606391)) ;
#49641=CARTESIAN_POINT('Origin',(0.,-1.91148346547618E-16,1.58079214606391)) ;
#49642=CARTESIAN_POINT('',(-0.272892694210214,1.03886703084701,0.756451169002388)) ;
#49643=CARTESIAN_POINT('Ctrl Pts',(-0.272892694210214,1.03886703084701,
0.756451169002387)) ;
#49644=CARTESIAN_POINT('Ctrl Pts',(-0.299689250637345,1.3071111559911,1.06273721049842)) ;
#49645=CARTESIAN_POINT('Ctrl Pts',(-0.345013184582945,1.75714893861133,
1.58079214606358)) ;
#49646=CARTESIAN_POINT('',(-0.465177703148305,0.465177703148315,0.277609509066653)) ;
#49647=CARTESIAN_POINT('Ctrl Pts',(-0.272892694210214,1.03886703084701,
0.756451169002388)) ;
#49648=CARTESIAN_POINT('Ctrl Pts',(-0.388126284358586,0.67608985904451,
0.386496290406958)) ;
#49649=CARTESIAN_POINT('Ctrl Pts',(-0.465177703148304,0.465177703148316,
0.277609509066654)) ;
#49650=CARTESIAN_POINT('',(-1.03886703084701,0.272892694210236,0.756451169002387)) ;
#49651=CARTESIAN_POINT('Ctrl Pts',(-0.465177703148307,0.465177703148314,
0.277609509066655)) ;
#49652=CARTESIAN_POINT('Ctrl Pts',(-0.676089859053593,0.38812628435528,
0.386496290411651)) ;
#49653=CARTESIAN_POINT('Ctrl Pts',(-1.03886703088336,0.272892694198688,
0.756451169039463)) ;
#49654=CARTESIAN_POINT('',(-1.75714893861161,0.34501318458301,1.58079214606391)) ;
#49655=CARTESIAN_POINT('Ctrl Pts',(-1.03886703084701,0.272892694210236,
0.756451169002386)) ;
#49656=CARTESIAN_POINT('Ctrl Pts',(-1.30711115599117,0.29968925063738,1.06273721049851)) ;
#49657=CARTESIAN_POINT('Ctrl Pts',(-1.75714893861161,0.34501318458301,1.58079214606391)) ;
#49658=CARTESIAN_POINT('',(-1.75714893861161,-0.345013184582992,1.58079214606391)) ;
#49659=CARTESIAN_POINT('Origin',(0.,1.91148346547618E-16,1.58079214606391)) ;
#49660=CARTESIAN_POINT('',(-1.03886703084701,-0.272892694210225,0.756451169002387)) ;
#49661=CARTESIAN_POINT('Ctrl Pts',(-1.03886703084701,-0.272892694210225,
0.756451169002387)) ;
#49662=CARTESIAN_POINT('Ctrl Pts',(-1.3071111559911,-0.299689250637359,
1.06273721049842)) ;
#49663=CARTESIAN_POINT('Ctrl Pts',(-1.75714893861132,-0.345013184582963,
1.58079214606358)) ;
#49664=CARTESIAN_POINT('',(-0.46517770314831,-0.465177703148309,0.277609509066653)) ;
#49665=CARTESIAN_POINT('Ctrl Pts',(-1.03886703084701,-0.272892694210225,
0.756451169002387)) ;
#49666=CARTESIAN_POINT('Ctrl Pts',(-0.676089859044505,-0.388126284358593,
0.386496290406956)) ;
#49667=CARTESIAN_POINT('Ctrl Pts',(-0.46517770314831,-0.465177703148309,
0.277609509066652)) ;
#49668=CARTESIAN_POINT('',(-0.272892694210225,-1.03886703084701,0.756451169002387)) ;
#49669=CARTESIAN_POINT('Ctrl Pts',(-0.465177703148309,-0.465177703148311,
0.277609509066654)) ;
#49670=CARTESIAN_POINT('Ctrl Pts',(-0.388126284355273,-0.676089859053595,
0.386496290411649)) ;
#49671=CARTESIAN_POINT('Ctrl Pts',(-0.272892694198678,-1.03886703088336,
0.756451169039458)) ;
#49672=CARTESIAN_POINT('',(-0.345013184582991,-1.75714893861161,1.58079214606391)) ;
#49673=CARTESIAN_POINT('Ctrl Pts',(-0.272892694210235,-1.038867030847,0.756451169002379)) ;
#49674=CARTESIAN_POINT('Ctrl Pts',(-0.299689250637379,-1.30711115599116,
1.0627372104985)) ;
#49675=CARTESIAN_POINT('Ctrl Pts',(-0.345013184583009,-1.75714893861159,
1.58079214606389)) ;
#49676=CARTESIAN_POINT('',(0.345013184582986,-1.75714893861161,1.58079214606391)) ;
#49677=CARTESIAN_POINT('Origin',(-1.91148346547618E-16,6.6739088492173E-31,
1.58079214606391)) ;
#49678=CARTESIAN_POINT('',(0.272892694210221,-1.03886703084701,0.756451169002387)) ;
#49679=CARTESIAN_POINT('Ctrl Pts',(0.272892694210226,-1.03886703084701,
0.756451169002393)) ;
#49680=CARTESIAN_POINT('Ctrl Pts',(0.299689250637368,-1.30711115599118,
1.06273721049852)) ;
#49681=CARTESIAN_POINT('Ctrl Pts',(0.345013184582994,-1.75714893861162,
1.58079214606392)) ;
#49682=CARTESIAN_POINT('',(0.465177703148308,-0.465177703148311,0.277609509066653)) ;
#49683=CARTESIAN_POINT('Ctrl Pts',(0.272892694198675,-1.03886703088336,
0.756451169039455)) ;
#49684=CARTESIAN_POINT('Ctrl Pts',(0.388126284355271,-0.676089859053595,
0.386496290411648)) ;
#49685=CARTESIAN_POINT('Ctrl Pts',(0.465177703148307,-0.465177703148311,
0.277609509066652)) ;
#49686=CARTESIAN_POINT('',(1.03886703084701,-0.272892694210228,0.756451169002387)) ;
#49687=CARTESIAN_POINT('Ctrl Pts',(0.465177703148308,-0.465177703148311,
0.277609509066653)) ;
#49688=CARTESIAN_POINT('Ctrl Pts',(0.676089859044505,-0.388126284358596,
0.386496290406957)) ;
#49689=CARTESIAN_POINT('Ctrl Pts',(1.03886703084701,-0.272892694210229,
0.756451169002387)) ;
#49690=CARTESIAN_POINT('',(1.75714893861161,-0.345013184582997,1.58079214606391)) ;
#49691=CARTESIAN_POINT('Ctrl Pts',(1.03886703084701,-0.272892694210228,
0.756451169002387)) ;
#49692=CARTESIAN_POINT('Ctrl Pts',(1.30711115599109,-0.299689250637364,
1.06273721049842)) ;
#49693=CARTESIAN_POINT('Ctrl Pts',(1.75714893861132,-0.345013184582969,
1.58079214606358)) ;
#49694=CARTESIAN_POINT('',(1.75714893861161,0.345013184582992,1.58079214606391)) ;
#49695=CARTESIAN_POINT('Origin',(0.,-1.91148346547618E-16,1.58079214606391)) ;
#49696=CARTESIAN_POINT('',(1.03886703084701,0.272892694210225,0.756451169002387)) ;
#49697=CARTESIAN_POINT('Ctrl Pts',(1.03886703084701,0.272892694210225,0.756451169002387)) ;
#49698=CARTESIAN_POINT('Ctrl Pts',(1.30711115599118,0.299689250637367,1.06273721049851)) ;
#49699=CARTESIAN_POINT('Ctrl Pts',(1.75714893861161,0.345013184582992,1.5807921460639)) ;
#49700=CARTESIAN_POINT('',(0.46517770314831,0.46517770314831,0.277609509066653)) ;
#49701=CARTESIAN_POINT('Ctrl Pts',(1.03886703088336,0.272892694198679,0.756451169039457)) ;
#49702=CARTESIAN_POINT('Ctrl Pts',(0.676089859053591,0.388126284355274,
0.386496290411646)) ;
#49703=CARTESIAN_POINT('Ctrl Pts',(0.465177703148306,0.465177703148311,
0.277609509066652)) ;
#49704=CARTESIAN_POINT('',(0.272892694210225,1.03886703084701,0.756451169002387)) ;
#49705=CARTESIAN_POINT('Ctrl Pts',(0.46517770314831,0.465177703148308,0.277609509066653)) ;
#49706=CARTESIAN_POINT('Ctrl Pts',(0.388126284358594,0.676089859044504,
0.386496290406956)) ;
#49707=CARTESIAN_POINT('Ctrl Pts',(0.272892694210225,1.03886703084701,0.756451169002387)) ;
#49708=CARTESIAN_POINT('',(0.345013184582991,1.75714893861161,1.58079214606391)) ;
#49709=CARTESIAN_POINT('Ctrl Pts',(0.272892694210225,1.03886703084701,0.756451169002387)) ;
#49710=CARTESIAN_POINT('Ctrl Pts',(0.299689250637359,1.30711115599109,1.06273721049842)) ;
#49711=CARTESIAN_POINT('Ctrl Pts',(0.345013184582963,1.75714893861132,1.58079214606358)) ;
#49712=CARTESIAN_POINT('Origin',(0.,-1.91148346547618E-16,1.58079214606391)) ;
#49713=CARTESIAN_POINT('Origin',(0.,-1.33894542197505E-16,-5.05771666666667)) ;
#49714=CARTESIAN_POINT('Origin',(0.,-1.33894542197505E-16,-2.36272659886193)) ;
#49715=CARTESIAN_POINT('Origin',(0.,-1.33894542197505E-16,-2.36272659886194)) ;
#49716=CARTESIAN_POINT('Origin',(0.,1.33894542197505E-16,-5.05771666666667)) ;
#49717=CARTESIAN_POINT('Origin',(0.,1.33894542197505E-16,-2.36272659886194)) ;
#49718=CARTESIAN_POINT('Origin',(0.,1.33894542197505E-16,-2.36272659886193)) ;
#49719=CARTESIAN_POINT('Origin',(-1.33894542197505E-16,4.67490295455533E-31,
-5.05771666666667)) ;
#49720=CARTESIAN_POINT('Origin',(-1.33894542197505E-16,4.67490295455533E-31,
-2.36272659886193)) ;
#49721=CARTESIAN_POINT('Origin',(-1.33894542197505E-16,4.67490295455533E-31,
-2.36272659886193)) ;
#49722=CARTESIAN_POINT('Origin',(0.280271407259434,-0.676635032551125,1.7018)) ;
#49723=CARTESIAN_POINT('',(0.559813216252793,-0.559813216252798,1.69090411891923)) ;
#49724=CARTESIAN_POINT('',(1.05500145698799,-0.354005931931581,1.68357971860376)) ;
#49725=CARTESIAN_POINT('Origin',(0.676635032551123,-0.280271407259438,1.7018)) ;
#49726=CARTESIAN_POINT('',(0.354005931931574,-1.05500145698799,1.68357971860376)) ;
#49727=CARTESIAN_POINT('Origin',(0.355600000000001,-1.18647113870949E-15,
1.7018)) ;
#49728=CARTESIAN_POINT('Origin',(-0.355600000000001,-1.10199250766261E-16,
1.7018)) ;
#49729=CARTESIAN_POINT('',(-0.354005931931577,-1.05500145698799,1.68357971860376)) ;
#49730=CARTESIAN_POINT('Origin',(-0.676635032551124,-0.280271407259437,
1.7018)) ;
#49731=CARTESIAN_POINT('',(-0.559813216252796,-0.559813216252795,1.69090411891923)) ;
#49732=CARTESIAN_POINT('Origin',(-0.280271407259436,-0.676635032551124,
1.7018)) ;
#49733=CARTESIAN_POINT('',(-1.05500145698799,-0.354005931931578,1.68357971860376)) ;
#49734=CARTESIAN_POINT('Origin',(5.50996253831303E-17,-0.355600000000001,
1.7018)) ;
#49735=CARTESIAN_POINT('Origin',(3.6145130415116E-15,0.355600000000001,
1.7018)) ;
#49736=CARTESIAN_POINT('',(-1.05500145698799,0.354005931931589,1.68357971860376)) ;
#49737=CARTESIAN_POINT('Origin',(-0.28027140725943,0.676635032551127,1.7018)) ;
#49738=CARTESIAN_POINT('',(-0.559813216252789,0.559813216252801,1.69090411891923)) ;
#49739=CARTESIAN_POINT('Origin',(-0.676635032551121,0.280271407259443,1.7018)) ;
#49740=CARTESIAN_POINT('',(-0.354005931931567,1.055001456988,1.68357971860376)) ;
#49741=CARTESIAN_POINT('Origin',(-0.355600000000001,3.66961266689473E-15,
1.7018)) ;
#49742=CARTESIAN_POINT('Origin',(0.,-1.33894542197505E-16,-2.36272659886193)) ;
#49743=CARTESIAN_POINT('Origin',(0.,-1.33894542197505E-16,-5.05771666666667)) ;
#49744=CARTESIAN_POINT('Origin',(0.,-1.33894542197505E-16,-2.36272659886194)) ;
#49745=CARTESIAN_POINT('Origin',(0.355600000000001,1.10199250766261E-16,
1.7018)) ;
#49746=CARTESIAN_POINT('',(0.354005931931577,1.05500145698799,1.68357971860376)) ;
#49747=CARTESIAN_POINT('Origin',(0.676635032551124,0.280271407259437,1.7018)) ;
#49748=CARTESIAN_POINT('',(0.559813216252796,0.559813216252795,1.69090411891923)) ;
#49749=CARTESIAN_POINT('Origin',(0.280271407259436,0.676635032551124,1.7018)) ;
#49750=CARTESIAN_POINT('',(1.05500145698799,0.354005931931578,1.68357971860376)) ;
#49751=CARTESIAN_POINT('Origin',(-5.50996253831303E-17,0.355600000000001,
1.7018)) ;
#49752=CARTESIAN_POINT('Origin',(-1.13137151332636E-15,-0.355600000000001,
1.7018)) ;
#49753=CARTESIAN_POINT('Origin',(0.,0.,0.)) ;
#49754=CARTESIAN_POINT('Ctrl Pts',(0.491435946297415,1.33480802765296,1.64178456984939E-16)) ;
#49755=CARTESIAN_POINT('Ctrl Pts',(0.631063497904959,1.26227785840513,1.57620625117627E-16)) ;
#49756=CARTESIAN_POINT('Ctrl Pts',(0.757237166432859,1.16646160759251,4.82074980013067E-17)) ;
#49757=CARTESIAN_POINT('Ctrl Pts',(0.973454042431244,0.93461893256702,2.5493608898663E-17)) ;
#49758=CARTESIAN_POINT('Ctrl Pts',(1.06120306904122,0.799873965737815,1.19234218146397E-16)) ;
#49759=CARTESIAN_POINT('Ctrl Pts',(1.15674989147546,0.576768217997932,9.6322737338553E-17)) ;
#49760=CARTESIAN_POINT('Ctrl Pts',(1.21968871378171,0.413792942784443,1.81740200073975E-18)) ;
#49761=CARTESIAN_POINT('Ctrl Pts',(1.22263774786217,0.0317209092632606,
-3.26382690937545E-17)) ;
#49762=CARTESIAN_POINT('Ctrl Pts',(1.19297461938357,-0.123873174315643,
8.71909996142948E-10)) ;
#49763=CARTESIAN_POINT('Ctrl Pts',(1.10615071765841,-0.338117862197598,
8.71909977118802E-10)) ;
#49764=CARTESIAN_POINT('Ctrl Pts',(1.07193711691856,-0.404128908965352,
-4.7408330026157E-17)) ;
#49765=CARTESIAN_POINT('Ctrl Pts',(0.975954116420733,-0.553514539862139,
-6.15088024485444E-17)) ;
#49766=CARTESIAN_POINT('Ctrl Pts',(0.923582668623707,-0.610351469100532,
6.3909699607946E-17)) ;
#49767=CARTESIAN_POINT('Ctrl Pts',(0.835080540402359,-0.703023782935501,
5.64767333076593E-17)) ;
#49768=CARTESIAN_POINT('Ctrl Pts',(0.759258426489408,-0.762791943082818,
1.79114405874878E-16)) ;
#49769=CARTESIAN_POINT('Ctrl Pts',(0.599973513232069,-0.855169615486292,
1.71874893413169E-16)) ;
#49770=CARTESIAN_POINT('Ctrl Pts',(0.518382068332362,-0.889218776095626,
-1.05380833470058E-16)) ;
#49771=CARTESIAN_POINT('Ctrl Pts',(0.433387415541747,-0.912241887310308,
-1.07462473344528E-16)) ;
#49772=CARTESIAN_POINT('Ctrl Pts',(-0.348937280953795,-0.947761935759142,
-1.09130430082023E-16)) ;
#49773=CARTESIAN_POINT('Ctrl Pts',(-0.447327671712729,-0.930286436395833,
-1.07550378803908E-16)) ;
#49774=CARTESIAN_POINT('Ctrl Pts',(-0.542596325781123,-0.898520691472632,
-3.93871915511075E-18)) ;
#49775=CARTESIAN_POINT('Ctrl Pts',(-0.728576337247976,-0.804661253243085,
4.27229455739307E-18)) ;
#49776=CARTESIAN_POINT('Ctrl Pts',(-0.816997845188147,-0.740844670056653,
-1.84590828456541E-16)) ;
#49777=CARTESIAN_POINT('Ctrl Pts',(-0.923212579592666,-0.635422833885916,
-1.75901819604059E-16)) ;
#49778=CARTESIAN_POINT('Ctrl Pts',(-0.976887238434203,-0.578692663218018,
-8.04035336178024E-18)) ;
#49779=CARTESIAN_POINT('Ctrl Pts',(-1.12225033728478,-0.360679713470414,
1.23482497677119E-17)) ;
#49780=CARTESIAN_POINT('Ctrl Pts',(-1.18348749295032,-0.212768435947515,
3.01208314832676E-16)) ;
#49781=CARTESIAN_POINT('Ctrl Pts',(-1.24366589458071,0.089532641158921,
3.29749778961003E-16)) ;
#49782=CARTESIAN_POINT('Ctrl Pts',(-1.24543419386366,0.240302910086207,
-4.39954125660478E-13)) ;
#49783=CARTESIAN_POINT('Ctrl Pts',(-1.18298227166626,0.599699993322773,
-4.39919613627758E-13)) ;
#49784=CARTESIAN_POINT('Ctrl Pts',(-1.09722247554694,0.7592012229505,-1.08314018284233E-16)) ;
#49785=CARTESIAN_POINT('Ctrl Pts',(-0.980276797203946,0.943575674806962,
-9.10890065762937E-17)) ;
#49786=CARTESIAN_POINT('Ctrl Pts',(-0.916929923265699,1.02290966726172,
-4.78134042320515E-16)) ;
#49787=CARTESIAN_POINT('Ctrl Pts',(-0.774264939856819,1.16639610296708,
-4.65847090734852E-16)) ;
#49788=CARTESIAN_POINT('Ctrl Pts',(-0.695420302659111,1.23011726595772,
9.13016138116806E-17)) ;
#49789=CARTESIAN_POINT('Ctrl Pts',(-0.610373744209535,1.28478233657676,
9.62441686940418E-17)) ;
#49790=CARTESIAN_POINT('Origin',(0.,0.92075,-3.85445)) ;
#49791=CARTESIAN_POINT('Ctrl Pts',(0.,1.00995540144767,-4.17195000000001)) ;
#49792=CARTESIAN_POINT('Ctrl Pts',(-0.583098022895331,1.00995540144767,
-4.11903333333334)) ;
#49793=CARTESIAN_POINT('Ctrl Pts',(-0.874647034342996,0.504977700723831,
-4.06611666666667)) ;
#49794=CARTESIAN_POINT('Ctrl Pts',(-1.16619604579066,-5.43898472251395E-15,
-4.01320000000001)) ;
#49795=CARTESIAN_POINT('Ctrl Pts',(-0.874647034342996,-0.504977700723842,
-3.96028333333334)) ;
#49796=CARTESIAN_POINT('Ctrl Pts',(-0.583098022895331,-1.00995540144768,
-3.90736666666667)) ;
#49797=CARTESIAN_POINT('Ctrl Pts',(-1.23683864966447E-16,-1.00995540144768,
-3.85445000000001)) ;
#49798=CARTESIAN_POINT('Ctrl Pts',(0.58309802289533,-1.00995540144768,-3.80153333333334)) ;
#49799=CARTESIAN_POINT('Ctrl Pts',(0.874647034342996,-0.504977700723843,
-3.74861666666667)) ;
#49800=CARTESIAN_POINT('Ctrl Pts',(1.16619604579066,-5.72462037344511E-15,
-3.69570000000001)) ;
#49801=CARTESIAN_POINT('Ctrl Pts',(0.874647034342997,0.504977700723831,
-3.64278333333334)) ;
#49802=CARTESIAN_POINT('Ctrl Pts',(0.583098022895331,1.00995540144767,-3.58986666666667)) ;
#49803=CARTESIAN_POINT('Ctrl Pts',(0.,1.00995540144767,-3.53695000000001)) ;
#49804=CARTESIAN_POINT('Ctrl Pts',(-0.583098022895331,1.00995540144767,
-3.48403333333334)) ;
#49805=CARTESIAN_POINT('Ctrl Pts',(-0.874647034342996,0.504977700723831,
-3.43111666666667)) ;
#49806=CARTESIAN_POINT('Ctrl Pts',(-1.16619604579066,-5.43898472251395E-15,
-3.37820000000001)) ;
#49807=CARTESIAN_POINT('Ctrl Pts',(-0.874647034342996,-0.504977700723842,
-3.32528333333334)) ;
#49808=CARTESIAN_POINT('Ctrl Pts',(-0.583098022895331,-1.00995540144768,
-3.27236666666667)) ;
#49809=CARTESIAN_POINT('Ctrl Pts',(-1.23683864966447E-16,-1.00995540144768,
-3.21945000000001)) ;
#49810=CARTESIAN_POINT('Ctrl Pts',(0.58309802289533,-1.00995540144768,-3.16653333333334)) ;
#49811=CARTESIAN_POINT('Ctrl Pts',(0.874647034342996,-0.504977700723843,
-3.11361666666667)) ;
#49812=CARTESIAN_POINT('Ctrl Pts',(1.16619604579066,-5.72462037344511E-15,
-3.06070000000001)) ;
#49813=CARTESIAN_POINT('Ctrl Pts',(0.874647034342997,0.504977700723831,
-3.00778333333334)) ;
#49814=CARTESIAN_POINT('Ctrl Pts',(0.583098022895331,1.00995540144767,-2.95486666666667)) ;
#49815=CARTESIAN_POINT('Ctrl Pts',(0.,1.00995540144767,-2.90195000000001)) ;
#49816=CARTESIAN_POINT('Ctrl Pts',(-0.583098022895331,1.00995540144767,
-2.84903333333334)) ;
#49817=CARTESIAN_POINT('Ctrl Pts',(-0.874647034342996,0.504977700723831,
-2.79611666666667)) ;
#49818=CARTESIAN_POINT('Ctrl Pts',(-1.16619604579066,-5.43898472251395E-15,
-2.74320000000001)) ;
#49819=CARTESIAN_POINT('Ctrl Pts',(-0.874647034342996,-0.504977700723842,
-2.69028333333334)) ;
#49820=CARTESIAN_POINT('Ctrl Pts',(-0.583098022895331,-1.00995540144768,
-2.63736666666667)) ;
#49821=CARTESIAN_POINT('Ctrl Pts',(-1.23683864966447E-16,-1.00995540144768,
-2.58445000000001)) ;
#49822=CARTESIAN_POINT('Ctrl Pts',(0.58309802289533,-1.00995540144768,-2.53153333333334)) ;
#49823=CARTESIAN_POINT('Ctrl Pts',(0.874647034342996,-0.504977700723843,
-2.47861666666667)) ;
#49824=CARTESIAN_POINT('Ctrl Pts',(1.16619604579066,-5.72462037344511E-15,
-2.42570000000001)) ;
#49825=CARTESIAN_POINT('Ctrl Pts',(0.874647034342997,0.504977700723831,
-2.37278333333334)) ;
#49826=CARTESIAN_POINT('Ctrl Pts',(0.583098022895331,1.00995540144767,-2.31986666666667)) ;
#49827=CARTESIAN_POINT('Ctrl Pts',(0.,1.00995540144767,-2.26695000000001)) ;
#49828=CARTESIAN_POINT('Ctrl Pts',(-0.583098022895331,1.00995540144767,
-2.21403333333334)) ;
#49829=CARTESIAN_POINT('Ctrl Pts',(-0.874647034342996,0.504977700723831,
-2.16111666666667)) ;
#49830=CARTESIAN_POINT('Ctrl Pts',(-1.16619604579066,-5.43898472251395E-15,
-2.10820000000001)) ;
#49831=CARTESIAN_POINT('Ctrl Pts',(-0.874647034342996,-0.504977700723842,
-2.05528333333334)) ;
#49832=CARTESIAN_POINT('Ctrl Pts',(-0.583098022895331,-1.00995540144768,
-2.00236666666667)) ;
#49833=CARTESIAN_POINT('Ctrl Pts',(-1.23683864966447E-16,-1.00995540144768,
-1.94945000000001)) ;
#49834=CARTESIAN_POINT('Ctrl Pts',(0.58309802289533,-1.00995540144768,-1.89653333333334)) ;
#49835=CARTESIAN_POINT('Ctrl Pts',(0.874647034342996,-0.504977700723843,
-1.84361666666667)) ;
#49836=CARTESIAN_POINT('Ctrl Pts',(1.16619604579066,-5.72462037344511E-15,
-1.79070000000001)) ;
#49837=CARTESIAN_POINT('Ctrl Pts',(0.874647034342997,0.504977700723831,
-1.73778333333334)) ;
#49838=CARTESIAN_POINT('Ctrl Pts',(0.583098022895331,1.00995540144767,-1.68486666666667)) ;
#49839=CARTESIAN_POINT('Ctrl Pts',(0.,1.00995540144767,-1.63195000000001)) ;
#49840=CARTESIAN_POINT('Ctrl Pts',(-0.583098022895331,1.00995540144767,
-1.57903333333334)) ;
#49841=CARTESIAN_POINT('Ctrl Pts',(-0.874647034342996,0.504977700723831,
-1.52611666666667)) ;
#49842=CARTESIAN_POINT('Ctrl Pts',(-1.16619604579066,-5.43898472251395E-15,
-1.47320000000001)) ;
#49843=CARTESIAN_POINT('Ctrl Pts',(-0.874647034342996,-0.504977700723842,
-1.42028333333334)) ;
#49844=CARTESIAN_POINT('Ctrl Pts',(-0.583098022895331,-1.00995540144768,
-1.36736666666667)) ;
#49845=CARTESIAN_POINT('Ctrl Pts',(-1.23683864966447E-16,-1.00995540144768,
-1.31445000000001)) ;
#49846=CARTESIAN_POINT('Ctrl Pts',(0.58309802289533,-1.00995540144768,-1.26153333333334)) ;
#49847=CARTESIAN_POINT('Ctrl Pts',(0.874647034342996,-0.504977700723843,
-1.20861666666667)) ;
#49848=CARTESIAN_POINT('Ctrl Pts',(1.16619604579066,-5.72462037344511E-15,
-1.15570000000001)) ;
#49849=CARTESIAN_POINT('Ctrl Pts',(0.874647034342997,0.504977700723831,
-1.10278333333334)) ;
#49850=CARTESIAN_POINT('Ctrl Pts',(0.583098022895331,1.00995540144767,-1.04986666666667)) ;
#49851=CARTESIAN_POINT('Ctrl Pts',(0.,1.00995540144767,-0.996950000000008)) ;
#49852=CARTESIAN_POINT('Ctrl Pts',(-0.583098022895331,1.00995540144767,
-0.944033333333341)) ;
#49853=CARTESIAN_POINT('Ctrl Pts',(-0.874647034342996,0.504977700723831,
-0.891116666666674)) ;
#49854=CARTESIAN_POINT('Ctrl Pts',(-1.16619604579066,-5.43898472251395E-15,
-0.838200000000008)) ;
#49855=CARTESIAN_POINT('Ctrl Pts',(-0.874647034342996,-0.504977700723842,
-0.785283333333341)) ;
#49856=CARTESIAN_POINT('Ctrl Pts',(-0.583098022895331,-1.00995540144768,
-0.732366666666674)) ;
#49857=CARTESIAN_POINT('Ctrl Pts',(-1.23683864966447E-16,-1.00995540144768,
-0.679450000000008)) ;
#49858=CARTESIAN_POINT('Ctrl Pts',(0.58309802289533,-1.00995540144768,-0.626533333333341)) ;
#49859=CARTESIAN_POINT('Ctrl Pts',(0.874647034342996,-0.504977700723843,
-0.573616666666674)) ;
#49860=CARTESIAN_POINT('Ctrl Pts',(1.16619604579066,-5.72462037344511E-15,
-0.520700000000008)) ;
#49861=CARTESIAN_POINT('Ctrl Pts',(0.874647034342997,0.504977700723831,
-0.467783333333341)) ;
#49862=CARTESIAN_POINT('Ctrl Pts',(0.583098022895331,1.00995540144767,-0.414866666666674)) ;
#49863=CARTESIAN_POINT('Ctrl Pts',(0.,1.00995540144767,-0.361950000000008)) ;
#49864=CARTESIAN_POINT('Ctrl Pts',(-0.583098022895331,1.00995540144767,
-0.309033333333341)) ;
#49865=CARTESIAN_POINT('Ctrl Pts',(-0.874647034342996,0.504977700723831,
-0.256116666666674)) ;
#49866=CARTESIAN_POINT('Ctrl Pts',(-1.16619604579066,-5.43898472251395E-15,
-0.203200000000008)) ;
#49867=CARTESIAN_POINT('Ctrl Pts',(-0.874647034342996,-0.504977700723842,
-0.150283333333341)) ;
#49868=CARTESIAN_POINT('Ctrl Pts',(-0.583098022895331,-1.00995540144768,
-0.0973666666666739)) ;
#49869=CARTESIAN_POINT('Ctrl Pts',(-1.23683864966447E-16,-1.00995540144768,
-0.0444500000000075)) ;
#49870=CARTESIAN_POINT('Ctrl Pts',(0.58309802289533,-1.00995540144768,0.00846666666665889)) ;
#49871=CARTESIAN_POINT('Ctrl Pts',(0.874647034342996,-0.504977700723843,
0.0613833333333261)) ;
#49872=CARTESIAN_POINT('Ctrl Pts',(1.16619604579066,-5.72462037344511E-15,
0.114299999999993)) ;
#49873=CARTESIAN_POINT('Ctrl Pts',(0.874647034342997,0.504977700723831,
0.167216666666659)) ;
#49874=CARTESIAN_POINT('Ctrl Pts',(0.583098022895331,1.00995540144767,0.220133333333326)) ;
#49875=CARTESIAN_POINT('Ctrl Pts',(0.,1.00995540144767,0.273049999999993)) ;
#49876=CARTESIAN_POINT('Ctrl Pts',(-0.583098022895331,1.00995540144767,
0.325966666666659)) ;
#49877=CARTESIAN_POINT('Ctrl Pts',(-0.874647034342996,0.504977700723831,
0.378883333333326)) ;
#49878=CARTESIAN_POINT('Ctrl Pts',(-1.16619604579066,-5.43898472251395E-15,
0.431799999999993)) ;
#49879=CARTESIAN_POINT('Ctrl Pts',(-0.874647034342996,-0.504977700723842,
0.484716666666659)) ;
#49880=CARTESIAN_POINT('Ctrl Pts',(-0.583098022895331,-1.00995540144768,
0.537633333333326)) ;
#49881=CARTESIAN_POINT('Ctrl Pts',(-1.23683864966447E-16,-1.00995540144768,
0.590549999999993)) ;
#49882=CARTESIAN_POINT('Ctrl Pts',(0.58309802289533,-1.00995540144768,0.643466666666659)) ;
#49883=CARTESIAN_POINT('Ctrl Pts',(0.874647034342996,-0.504977700723843,
0.696383333333326)) ;
#49884=CARTESIAN_POINT('Ctrl Pts',(1.16619604579066,-5.72462037344511E-15,
0.749299999999993)) ;
#49885=CARTESIAN_POINT('Ctrl Pts',(0.874647034342997,0.504977700723831,
0.802216666666659)) ;
#49886=CARTESIAN_POINT('Ctrl Pts',(0.583098022895331,1.00995540144767,0.855133333333326)) ;
#49887=CARTESIAN_POINT('Ctrl Pts',(0.,1.00995540144767,0.908049999999993)) ;
#49888=CARTESIAN_POINT('Ctrl Pts',(-0.583098022895331,1.00995540144767,
0.960966666666659)) ;
#49889=CARTESIAN_POINT('Ctrl Pts',(-0.874647034342996,0.504977700723831,
1.01388333333333)) ;
#49890=CARTESIAN_POINT('Ctrl Pts',(-1.16619604579066,-5.43898472251395E-15,
1.06679999999999)) ;
#49891=CARTESIAN_POINT('Ctrl Pts',(-0.874647034342996,-0.504977700723842,
1.11971666666666)) ;
#49892=CARTESIAN_POINT('Ctrl Pts',(-0.583098022895331,-1.00995540144768,
1.17263333333333)) ;
#49893=CARTESIAN_POINT('Ctrl Pts',(-1.23683864966447E-16,-1.00995540144768,
1.22554999999999)) ;
#49894=CARTESIAN_POINT('Ctrl Pts',(0.58309802289533,-1.00995540144768,1.27846666666666)) ;
#49895=CARTESIAN_POINT('Ctrl Pts',(0.874647034342996,-0.504977700723843,
1.33138333333333)) ;
#49896=CARTESIAN_POINT('Ctrl Pts',(1.00995540144771,-0.2706167342093,1.35594204380104)) ;
#49897=CARTESIAN_POINT('Ctrl Pts',(1.00995540144767,1.23844880459077E-13,
1.38430000000001)) ;
#49898=CARTESIAN_POINT('Ctrl Pts',(0.,1.4567703832127,-4.42991875000001)) ;
#49899=CARTESIAN_POINT('Ctrl Pts',(-0.841066772895328,1.4567703832127,-4.37700208333334)) ;
#49900=CARTESIAN_POINT('Ctrl Pts',(-1.26160015934299,0.728385191606346,
-4.32408541666667)) ;
#49901=CARTESIAN_POINT('Ctrl Pts',(-1.68213354579066,-5.40739266211719E-15,
-4.27116875)) ;
#49902=CARTESIAN_POINT('Ctrl Pts',(-1.26160015934299,-0.728385191606357,
-4.21825208333334)) ;
#49903=CARTESIAN_POINT('Ctrl Pts',(-0.841066772895329,-1.45677038321271,
-4.16533541666667)) ;
#49904=CARTESIAN_POINT('Ctrl Pts',(-1.7840291868941E-16,-1.45677038321271,
-4.11241875)) ;
#49905=CARTESIAN_POINT('Ctrl Pts',(0.841066772895328,-1.45677038321271,
-4.05950208333334)) ;
#49906=CARTESIAN_POINT('Ctrl Pts',(1.26160015934299,-0.728385191606358,
-4.00658541666667)) ;
#49907=CARTESIAN_POINT('Ctrl Pts',(1.68213354579066,-5.81939655463538E-15,
-3.95366875000001)) ;
#49908=CARTESIAN_POINT('Ctrl Pts',(1.26160015934299,0.728385191606345,-3.90075208333334)) ;
#49909=CARTESIAN_POINT('Ctrl Pts',(0.841066772895329,1.4567703832127,-3.84783541666667)) ;
#49910=CARTESIAN_POINT('Ctrl Pts',(0.,1.4567703832127,-3.79491875)) ;
#49911=CARTESIAN_POINT('Ctrl Pts',(-0.841066772895328,1.4567703832127,-3.74200208333334)) ;
#49912=CARTESIAN_POINT('Ctrl Pts',(-1.26160015934299,0.728385191606346,
-3.68908541666667)) ;
#49913=CARTESIAN_POINT('Ctrl Pts',(-1.68213354579066,-5.40739266211719E-15,
-3.63616875)) ;
#49914=CARTESIAN_POINT('Ctrl Pts',(-1.26160015934299,-0.728385191606357,
-3.58325208333334)) ;
#49915=CARTESIAN_POINT('Ctrl Pts',(-0.841066772895329,-1.45677038321271,
-3.53033541666667)) ;
#49916=CARTESIAN_POINT('Ctrl Pts',(-1.7840291868941E-16,-1.45677038321271,
-3.47741875)) ;
#49917=CARTESIAN_POINT('Ctrl Pts',(0.841066772895328,-1.45677038321271,
-3.42450208333334)) ;
#49918=CARTESIAN_POINT('Ctrl Pts',(1.26160015934299,-0.728385191606358,
-3.37158541666667)) ;
#49919=CARTESIAN_POINT('Ctrl Pts',(1.68213354579066,-5.81939655463538E-15,
-3.31866875)) ;
#49920=CARTESIAN_POINT('Ctrl Pts',(1.26160015934299,0.728385191606345,-3.26575208333334)) ;
#49921=CARTESIAN_POINT('Ctrl Pts',(0.841066772895329,1.4567703832127,-3.21283541666667)) ;
#49922=CARTESIAN_POINT('Ctrl Pts',(0.,1.4567703832127,-3.15991875)) ;
#49923=CARTESIAN_POINT('Ctrl Pts',(-0.841066772895328,1.4567703832127,-3.10700208333334)) ;
#49924=CARTESIAN_POINT('Ctrl Pts',(-1.26160015934299,0.728385191606346,
-3.05408541666667)) ;
#49925=CARTESIAN_POINT('Ctrl Pts',(-1.68213354579066,-5.40739266211719E-15,
-3.00116875)) ;
#49926=CARTESIAN_POINT('Ctrl Pts',(-1.26160015934299,-0.728385191606357,
-2.94825208333334)) ;
#49927=CARTESIAN_POINT('Ctrl Pts',(-0.841066772895329,-1.45677038321271,
-2.89533541666667)) ;
#49928=CARTESIAN_POINT('Ctrl Pts',(-1.7840291868941E-16,-1.45677038321271,
-2.84241875)) ;
#49929=CARTESIAN_POINT('Ctrl Pts',(0.841066772895328,-1.45677038321271,
-2.78950208333334)) ;
#49930=CARTESIAN_POINT('Ctrl Pts',(1.26160015934299,-0.728385191606358,
-2.73658541666667)) ;
#49931=CARTESIAN_POINT('Ctrl Pts',(1.68213354579066,-5.81939655463538E-15,
-2.68366875)) ;
#49932=CARTESIAN_POINT('Ctrl Pts',(1.26160015934299,0.728385191606345,-2.63075208333334)) ;
#49933=CARTESIAN_POINT('Ctrl Pts',(0.841066772895329,1.4567703832127,-2.57783541666667)) ;
#49934=CARTESIAN_POINT('Ctrl Pts',(0.,1.4567703832127,-2.52491875)) ;
#49935=CARTESIAN_POINT('Ctrl Pts',(-0.841066772895328,1.4567703832127,-2.47200208333334)) ;
#49936=CARTESIAN_POINT('Ctrl Pts',(-1.26160015934299,0.728385191606346,
-2.41908541666667)) ;
#49937=CARTESIAN_POINT('Ctrl Pts',(-1.68213354579066,-5.40739266211719E-15,
-2.36616875)) ;
#49938=CARTESIAN_POINT('Ctrl Pts',(-1.26160015934299,-0.728385191606357,
-2.31325208333334)) ;
#49939=CARTESIAN_POINT('Ctrl Pts',(-0.841066772895329,-1.45677038321271,
-2.26033541666667)) ;
#49940=CARTESIAN_POINT('Ctrl Pts',(-1.7840291868941E-16,-1.45677038321271,
-2.20741875)) ;
#49941=CARTESIAN_POINT('Ctrl Pts',(0.841066772895328,-1.45677038321271,
-2.15450208333334)) ;
#49942=CARTESIAN_POINT('Ctrl Pts',(1.26160015934299,-0.728385191606358,
-2.10158541666667)) ;
#49943=CARTESIAN_POINT('Ctrl Pts',(1.68213354579066,-5.81939655463538E-15,
-2.04866875)) ;
#49944=CARTESIAN_POINT('Ctrl Pts',(1.26160015934299,0.728385191606345,-1.99575208333334)) ;
#49945=CARTESIAN_POINT('Ctrl Pts',(0.841066772895329,1.4567703832127,-1.94283541666667)) ;
#49946=CARTESIAN_POINT('Ctrl Pts',(0.,1.4567703832127,-1.88991875)) ;
#49947=CARTESIAN_POINT('Ctrl Pts',(-0.841066772895328,1.4567703832127,-1.83700208333334)) ;
#49948=CARTESIAN_POINT('Ctrl Pts',(-1.26160015934299,0.728385191606346,
-1.78408541666667)) ;
#49949=CARTESIAN_POINT('Ctrl Pts',(-1.68213354579066,-5.40739266211719E-15,
-1.73116875)) ;
#49950=CARTESIAN_POINT('Ctrl Pts',(-1.26160015934299,-0.728385191606357,
-1.67825208333334)) ;
#49951=CARTESIAN_POINT('Ctrl Pts',(-0.841066772895329,-1.45677038321271,
-1.62533541666667)) ;
#49952=CARTESIAN_POINT('Ctrl Pts',(-1.7840291868941E-16,-1.45677038321271,
-1.57241875)) ;
#49953=CARTESIAN_POINT('Ctrl Pts',(0.841066772895328,-1.45677038321271,
-1.51950208333334)) ;
#49954=CARTESIAN_POINT('Ctrl Pts',(1.26160015934299,-0.728385191606358,
-1.46658541666667)) ;
#49955=CARTESIAN_POINT('Ctrl Pts',(1.68213354579066,-5.81939655463538E-15,
-1.41366875)) ;
#49956=CARTESIAN_POINT('Ctrl Pts',(1.26160015934299,0.728385191606345,-1.36075208333334)) ;
#49957=CARTESIAN_POINT('Ctrl Pts',(0.841066772895329,1.4567703832127,-1.30783541666667)) ;
#49958=CARTESIAN_POINT('Ctrl Pts',(0.,1.4567703832127,-1.25491875)) ;
#49959=CARTESIAN_POINT('Ctrl Pts',(-0.841066772895328,1.4567703832127,-1.20200208333334)) ;
#49960=CARTESIAN_POINT('Ctrl Pts',(-1.26160015934299,0.728385191606346,
-1.14908541666667)) ;
#49961=CARTESIAN_POINT('Ctrl Pts',(-1.68213354579066,-5.40739266211719E-15,
-1.09616875)) ;
#49962=CARTESIAN_POINT('Ctrl Pts',(-1.26160015934299,-0.728385191606357,
-1.04325208333334)) ;
#49963=CARTESIAN_POINT('Ctrl Pts',(-0.841066772895329,-1.45677038321271,
-0.990335416666671)) ;
#49964=CARTESIAN_POINT('Ctrl Pts',(-1.7840291868941E-16,-1.45677038321271,
-0.937418750000005)) ;
#49965=CARTESIAN_POINT('Ctrl Pts',(0.841066772895328,-1.45677038321271,
-0.884502083333338)) ;
#49966=CARTESIAN_POINT('Ctrl Pts',(1.26160015934299,-0.728385191606358,
-0.831585416666671)) ;
#49967=CARTESIAN_POINT('Ctrl Pts',(1.68213354579066,-5.81939655463538E-15,
-0.778668750000004)) ;
#49968=CARTESIAN_POINT('Ctrl Pts',(1.26160015934299,0.728385191606345,-0.725752083333338)) ;
#49969=CARTESIAN_POINT('Ctrl Pts',(0.841066772895329,1.4567703832127,-0.672835416666671)) ;
#49970=CARTESIAN_POINT('Ctrl Pts',(0.,1.4567703832127,-0.619918750000005)) ;
#49971=CARTESIAN_POINT('Ctrl Pts',(-0.841066772895328,1.4567703832127,-0.567002083333338)) ;
#49972=CARTESIAN_POINT('Ctrl Pts',(-1.26160015934299,0.728385191606346,
-0.514085416666671)) ;
#49973=CARTESIAN_POINT('Ctrl Pts',(-1.68213354579066,-5.40739266211719E-15,
-0.461168750000004)) ;
#49974=CARTESIAN_POINT('Ctrl Pts',(-1.26160015934299,-0.728385191606357,
-0.408252083333338)) ;
#49975=CARTESIAN_POINT('Ctrl Pts',(-0.841066772895329,-1.45677038321271,
-0.355335416666671)) ;
#49976=CARTESIAN_POINT('Ctrl Pts',(-1.7840291868941E-16,-1.45677038321271,
-0.302418750000004)) ;
#49977=CARTESIAN_POINT('Ctrl Pts',(0.841066772895328,-1.45677038321271,
-0.249502083333338)) ;
#49978=CARTESIAN_POINT('Ctrl Pts',(1.26160015934299,-0.728385191606358,
-0.196585416666671)) ;
#49979=CARTESIAN_POINT('Ctrl Pts',(1.68213354579066,-5.81939655463538E-15,
-0.143668750000004)) ;
#49980=CARTESIAN_POINT('Ctrl Pts',(1.26160015934299,0.728385191606345,-0.090752083333338)) ;
#49981=CARTESIAN_POINT('Ctrl Pts',(0.841066772895329,1.4567703832127,-0.0378354166666707)) ;
#49982=CARTESIAN_POINT('Ctrl Pts',(0.,1.4567703832127,0.0150812499999957)) ;
#49983=CARTESIAN_POINT('Ctrl Pts',(-0.841066772895328,1.4567703832127,0.0679979166666621)) ;
#49984=CARTESIAN_POINT('Ctrl Pts',(-1.26160015934299,0.728385191606346,
0.120914583333329)) ;
#49985=CARTESIAN_POINT('Ctrl Pts',(-1.68213354579066,-5.40739266211719E-15,
0.173831249999996)) ;
#49986=CARTESIAN_POINT('Ctrl Pts',(-1.26160015934299,-0.728385191606357,
0.226747916666662)) ;
#49987=CARTESIAN_POINT('Ctrl Pts',(-0.841066772895329,-1.45677038321271,
0.279664583333329)) ;
#49988=CARTESIAN_POINT('Ctrl Pts',(-1.7840291868941E-16,-1.45677038321271,
0.332581249999996)) ;
#49989=CARTESIAN_POINT('Ctrl Pts',(0.841066772895328,-1.45677038321271,
0.385497916666662)) ;
#49990=CARTESIAN_POINT('Ctrl Pts',(1.26160015934299,-0.728385191606358,
0.438414583333329)) ;
#49991=CARTESIAN_POINT('Ctrl Pts',(1.68213354579066,-5.81939655463538E-15,
0.491331249999996)) ;
#49992=CARTESIAN_POINT('Ctrl Pts',(1.26160015934299,0.728385191606345,0.544247916666662)) ;
#49993=CARTESIAN_POINT('Ctrl Pts',(0.841066772895329,1.4567703832127,0.597164583333328)) ;
#49994=CARTESIAN_POINT('Ctrl Pts',(0.,1.4567703832127,0.650081249999996)) ;
#49995=CARTESIAN_POINT('Ctrl Pts',(-0.841066772895328,1.4567703832127,0.702997916666662)) ;
#49996=CARTESIAN_POINT('Ctrl Pts',(-1.26160015934299,0.728385191606346,
0.755914583333329)) ;
#49997=CARTESIAN_POINT('Ctrl Pts',(-1.68213354579066,-5.40739266211719E-15,
0.808831249999996)) ;
#49998=CARTESIAN_POINT('Ctrl Pts',(-1.26160015934299,-0.728385191606357,
0.861747916666662)) ;
#49999=CARTESIAN_POINT('Ctrl Pts',(-0.841066772895329,-1.45677038321271,
0.914664583333328)) ;
#50000=CARTESIAN_POINT('Ctrl Pts',(-1.7840291868941E-16,-1.45677038321271,
0.967581249999996)) ;
#50001=CARTESIAN_POINT('Ctrl Pts',(0.841066772895328,-1.45677038321271,
1.02049791666666)) ;
#50002=CARTESIAN_POINT('Ctrl Pts',(1.26160015934299,-0.728385191606358,
1.07341458333333)) ;
#50003=CARTESIAN_POINT('Ctrl Pts',(1.45677038321275,-0.39034044773934,1.09797329380104)) ;
#50004=CARTESIAN_POINT('Ctrl Pts',(1.4567703832127,1.81104617588996E-13,
1.12633125000001)) ;
#50005=CARTESIAN_POINT('Ctrl Pts',(0.,1.4567703832127,-3.83460625)) ;
#50006=CARTESIAN_POINT('Ctrl Pts',(-0.841066772895328,1.4567703832127,-3.78168958333334)) ;
#50007=CARTESIAN_POINT('Ctrl Pts',(-1.26160015934299,0.728385191606346,
-3.72877291666667)) ;
#50008=CARTESIAN_POINT('Ctrl Pts',(-1.68213354579066,-5.40739266211719E-15,
-3.67585625)) ;
#50009=CARTESIAN_POINT('Ctrl Pts',(-1.26160015934299,-0.728385191606357,
-3.62293958333334)) ;
#50010=CARTESIAN_POINT('Ctrl Pts',(-0.841066772895329,-1.45677038321271,
-3.57002291666667)) ;
#50011=CARTESIAN_POINT('Ctrl Pts',(-1.7840291868941E-16,-1.45677038321271,
-3.51710625)) ;
#50012=CARTESIAN_POINT('Ctrl Pts',(0.841066772895328,-1.45677038321271,
-3.46418958333334)) ;
#50013=CARTESIAN_POINT('Ctrl Pts',(1.26160015934299,-0.728385191606358,
-3.41127291666667)) ;
#50014=CARTESIAN_POINT('Ctrl Pts',(1.68213354579066,-5.81939655463538E-15,
-3.35835625)) ;
#50015=CARTESIAN_POINT('Ctrl Pts',(1.26160015934299,0.728385191606345,-3.30543958333334)) ;
#50016=CARTESIAN_POINT('Ctrl Pts',(0.841066772895329,1.4567703832127,-3.25252291666667)) ;
#50017=CARTESIAN_POINT('Ctrl Pts',(0.,1.4567703832127,-3.19960625)) ;
#50018=CARTESIAN_POINT('Ctrl Pts',(-0.841066772895328,1.4567703832127,-3.14668958333334)) ;
#50019=CARTESIAN_POINT('Ctrl Pts',(-1.26160015934299,0.728385191606346,
-3.09377291666667)) ;
#50020=CARTESIAN_POINT('Ctrl Pts',(-1.68213354579066,-5.40739266211719E-15,
-3.04085625)) ;
#50021=CARTESIAN_POINT('Ctrl Pts',(-1.26160015934299,-0.728385191606357,
-2.98793958333334)) ;
#50022=CARTESIAN_POINT('Ctrl Pts',(-0.841066772895329,-1.45677038321271,
-2.93502291666667)) ;
#50023=CARTESIAN_POINT('Ctrl Pts',(-1.7840291868941E-16,-1.45677038321271,
-2.88210625)) ;
#50024=CARTESIAN_POINT('Ctrl Pts',(0.841066772895328,-1.45677038321271,
-2.82918958333334)) ;
#50025=CARTESIAN_POINT('Ctrl Pts',(1.26160015934299,-0.728385191606358,
-2.77627291666667)) ;
#50026=CARTESIAN_POINT('Ctrl Pts',(1.68213354579066,-5.81939655463538E-15,
-2.72335625)) ;
#50027=CARTESIAN_POINT('Ctrl Pts',(1.26160015934299,0.728385191606345,-2.67043958333334)) ;
#50028=CARTESIAN_POINT('Ctrl Pts',(0.841066772895329,1.4567703832127,-2.61752291666667)) ;
#50029=CARTESIAN_POINT('Ctrl Pts',(0.,1.4567703832127,-2.56460625)) ;
#50030=CARTESIAN_POINT('Ctrl Pts',(-0.841066772895328,1.4567703832127,-2.51168958333334)) ;
#50031=CARTESIAN_POINT('Ctrl Pts',(-1.26160015934299,0.728385191606346,
-2.45877291666667)) ;
#50032=CARTESIAN_POINT('Ctrl Pts',(-1.68213354579066,-5.40739266211719E-15,
-2.40585625)) ;
#50033=CARTESIAN_POINT('Ctrl Pts',(-1.26160015934299,-0.728385191606357,
-2.35293958333334)) ;
#50034=CARTESIAN_POINT('Ctrl Pts',(-0.841066772895329,-1.45677038321271,
-2.30002291666667)) ;
#50035=CARTESIAN_POINT('Ctrl Pts',(-1.7840291868941E-16,-1.45677038321271,
-2.24710625)) ;
#50036=CARTESIAN_POINT('Ctrl Pts',(0.841066772895328,-1.45677038321271,
-2.19418958333334)) ;
#50037=CARTESIAN_POINT('Ctrl Pts',(1.26160015934299,-0.728385191606358,
-2.14127291666667)) ;
#50038=CARTESIAN_POINT('Ctrl Pts',(1.68213354579066,-5.81939655463538E-15,
-2.08835625)) ;
#50039=CARTESIAN_POINT('Ctrl Pts',(1.26160015934299,0.728385191606345,-2.03543958333334)) ;
#50040=CARTESIAN_POINT('Ctrl Pts',(0.841066772895329,1.4567703832127,-1.98252291666667)) ;
#50041=CARTESIAN_POINT('Ctrl Pts',(0.,1.4567703832127,-1.92960625)) ;
#50042=CARTESIAN_POINT('Ctrl Pts',(-0.841066772895328,1.4567703832127,-1.87668958333334)) ;
#50043=CARTESIAN_POINT('Ctrl Pts',(-1.26160015934299,0.728385191606346,
-1.82377291666667)) ;
#50044=CARTESIAN_POINT('Ctrl Pts',(-1.68213354579066,-5.40739266211719E-15,
-1.77085625)) ;
#50045=CARTESIAN_POINT('Ctrl Pts',(-1.26160015934299,-0.728385191606357,
-1.71793958333334)) ;
#50046=CARTESIAN_POINT('Ctrl Pts',(-0.841066772895329,-1.45677038321271,
-1.66502291666667)) ;
#50047=CARTESIAN_POINT('Ctrl Pts',(-1.7840291868941E-16,-1.45677038321271,
-1.61210625)) ;
#50048=CARTESIAN_POINT('Ctrl Pts',(0.841066772895328,-1.45677038321271,
-1.55918958333334)) ;
#50049=CARTESIAN_POINT('Ctrl Pts',(1.26160015934299,-0.728385191606358,
-1.50627291666667)) ;
#50050=CARTESIAN_POINT('Ctrl Pts',(1.68213354579066,-5.81939655463538E-15,
-1.45335625)) ;
#50051=CARTESIAN_POINT('Ctrl Pts',(1.26160015934299,0.728385191606345,-1.40043958333334)) ;
#50052=CARTESIAN_POINT('Ctrl Pts',(0.841066772895329,1.4567703832127,-1.34752291666667)) ;
#50053=CARTESIAN_POINT('Ctrl Pts',(0.,1.4567703832127,-1.29460625)) ;
#50054=CARTESIAN_POINT('Ctrl Pts',(-0.841066772895328,1.4567703832127,-1.24168958333334)) ;
#50055=CARTESIAN_POINT('Ctrl Pts',(-1.26160015934299,0.728385191606346,
-1.18877291666667)) ;
#50056=CARTESIAN_POINT('Ctrl Pts',(-1.68213354579066,-5.40739266211719E-15,
-1.13585625)) ;
#50057=CARTESIAN_POINT('Ctrl Pts',(-1.26160015934299,-0.728385191606357,
-1.08293958333334)) ;
#50058=CARTESIAN_POINT('Ctrl Pts',(-0.841066772895329,-1.45677038321271,
-1.03002291666667)) ;
#50059=CARTESIAN_POINT('Ctrl Pts',(-1.7840291868941E-16,-1.45677038321271,
-0.977106250000004)) ;
#50060=CARTESIAN_POINT('Ctrl Pts',(0.841066772895328,-1.45677038321271,
-0.924189583333337)) ;
#50061=CARTESIAN_POINT('Ctrl Pts',(1.26160015934299,-0.728385191606358,
-0.871272916666671)) ;
#50062=CARTESIAN_POINT('Ctrl Pts',(1.68213354579066,-5.81939655463538E-15,
-0.818356250000004)) ;
#50063=CARTESIAN_POINT('Ctrl Pts',(1.26160015934299,0.728385191606345,-0.765439583333338)) ;
#50064=CARTESIAN_POINT('Ctrl Pts',(0.841066772895329,1.4567703832127,-0.712522916666671)) ;
#50065=CARTESIAN_POINT('Ctrl Pts',(0.,1.4567703832127,-0.659606250000004)) ;
#50066=CARTESIAN_POINT('Ctrl Pts',(-0.841066772895328,1.4567703832127,-0.606689583333337)) ;
#50067=CARTESIAN_POINT('Ctrl Pts',(-1.26160015934299,0.728385191606346,
-0.553772916666671)) ;
#50068=CARTESIAN_POINT('Ctrl Pts',(-1.68213354579066,-5.40739266211719E-15,
-0.500856250000004)) ;
#50069=CARTESIAN_POINT('Ctrl Pts',(-1.26160015934299,-0.728385191606357,
-0.447939583333337)) ;
#50070=CARTESIAN_POINT('Ctrl Pts',(-0.841066772895329,-1.45677038321271,
-0.395022916666671)) ;
#50071=CARTESIAN_POINT('Ctrl Pts',(-1.7840291868941E-16,-1.45677038321271,
-0.342106250000004)) ;
#50072=CARTESIAN_POINT('Ctrl Pts',(0.841066772895328,-1.45677038321271,
-0.289189583333337)) ;
#50073=CARTESIAN_POINT('Ctrl Pts',(1.26160015934299,-0.728385191606358,
-0.236272916666671)) ;
#50074=CARTESIAN_POINT('Ctrl Pts',(1.68213354579066,-5.81939655463538E-15,
-0.183356250000004)) ;
#50075=CARTESIAN_POINT('Ctrl Pts',(1.26160015934299,0.728385191606345,-0.130439583333337)) ;
#50076=CARTESIAN_POINT('Ctrl Pts',(0.841066772895329,1.4567703832127,-0.077522916666671)) ;
#50077=CARTESIAN_POINT('Ctrl Pts',(0.,1.4567703832127,-0.0246062500000041)) ;
#50078=CARTESIAN_POINT('Ctrl Pts',(-0.841066772895328,1.4567703832127,0.0283104166666627)) ;
#50079=CARTESIAN_POINT('Ctrl Pts',(-1.26160015934299,0.728385191606346,
0.0812270833333295)) ;
#50080=CARTESIAN_POINT('Ctrl Pts',(-1.68213354579066,-5.40739266211719E-15,
0.134143749999996)) ;
#50081=CARTESIAN_POINT('Ctrl Pts',(-1.26160015934299,-0.728385191606357,
0.187060416666662)) ;
#50082=CARTESIAN_POINT('Ctrl Pts',(-0.841066772895329,-1.45677038321271,
0.23997708333333)) ;
#50083=CARTESIAN_POINT('Ctrl Pts',(-1.7840291868941E-16,-1.45677038321271,
0.292893749999996)) ;
#50084=CARTESIAN_POINT('Ctrl Pts',(0.841066772895328,-1.45677038321271,
0.345810416666662)) ;
#50085=CARTESIAN_POINT('Ctrl Pts',(1.26160015934299,-0.728385191606358,
0.39872708333333)) ;
#50086=CARTESIAN_POINT('Ctrl Pts',(1.68213354579066,-5.81939655463538E-15,
0.451643749999996)) ;
#50087=CARTESIAN_POINT('Ctrl Pts',(1.26160015934299,0.728385191606345,0.504560416666662)) ;
#50088=CARTESIAN_POINT('Ctrl Pts',(0.841066772895329,1.4567703832127,0.55747708333333)) ;
#50089=CARTESIAN_POINT('Ctrl Pts',(0.,1.4567703832127,0.610393749999996)) ;
#50090=CARTESIAN_POINT('Ctrl Pts',(-0.841066772895328,1.4567703832127,0.663310416666662)) ;
#50091=CARTESIAN_POINT('Ctrl Pts',(-1.26160015934299,0.728385191606346,
0.71622708333333)) ;
#50092=CARTESIAN_POINT('Ctrl Pts',(-1.68213354579066,-5.40739266211719E-15,
0.769143749999996)) ;
#50093=CARTESIAN_POINT('Ctrl Pts',(-1.26160015934299,-0.728385191606357,
0.822060416666662)) ;
#50094=CARTESIAN_POINT('Ctrl Pts',(-0.841066772895329,-1.45677038321271,
0.87497708333333)) ;
#50095=CARTESIAN_POINT('Ctrl Pts',(-1.7840291868941E-16,-1.45677038321271,
0.927893749999996)) ;
#50096=CARTESIAN_POINT('Ctrl Pts',(0.841066772895328,-1.45677038321271,
0.980810416666662)) ;
#50097=CARTESIAN_POINT('Ctrl Pts',(1.26160015934299,-0.728385191606358,
1.03372708333333)) ;
#50098=CARTESIAN_POINT('Ctrl Pts',(1.68213354579066,-5.81939655463538E-15,
1.08664375)) ;
#50099=CARTESIAN_POINT('Ctrl Pts',(1.26160015934299,0.728385191606345,1.13956041666666)) ;
#50100=CARTESIAN_POINT('Ctrl Pts',(0.841066772895329,1.4567703832127,1.19247708333333)) ;
#50101=CARTESIAN_POINT('Ctrl Pts',(0.,1.4567703832127,1.24539375)) ;
#50102=CARTESIAN_POINT('Ctrl Pts',(-0.841066772895328,1.4567703832127,1.29831041666666)) ;
#50103=CARTESIAN_POINT('Ctrl Pts',(-1.26160015934299,0.728385191606346,
1.35122708333333)) ;
#50104=CARTESIAN_POINT('Ctrl Pts',(-1.68213354579066,-5.40739266211719E-15,
1.40414375)) ;
#50105=CARTESIAN_POINT('Ctrl Pts',(-1.26160015934299,-0.728385191606357,
1.45706041666666)) ;
#50106=CARTESIAN_POINT('Ctrl Pts',(-0.841066772895329,-1.45677038321271,
1.50997708333333)) ;
#50107=CARTESIAN_POINT('Ctrl Pts',(-1.7840291868941E-16,-1.45677038321271,
1.56289375)) ;
#50108=CARTESIAN_POINT('Ctrl Pts',(0.841066772895328,-1.45677038321271,
1.61581041666666)) ;
#50109=CARTESIAN_POINT('Ctrl Pts',(1.26160015934299,-0.728385191606358,
1.66872708333333)) ;
#50110=CARTESIAN_POINT('Ctrl Pts',(1.45677038321276,-0.390340447739336,
1.69328579380104)) ;
#50111=CARTESIAN_POINT('Ctrl Pts',(1.4567703832127,1.90517177117201E-13,
1.72164375000001)) ;
#50112=CARTESIAN_POINT('Ctrl Pts',(0.,1.00995540144767,-4.092575)) ;
#50113=CARTESIAN_POINT('Ctrl Pts',(-0.583098022895331,1.00995540144767,
-4.03965833333334)) ;
#50114=CARTESIAN_POINT('Ctrl Pts',(-0.874647034342996,0.504977700723831,
-3.98674166666667)) ;
#50115=CARTESIAN_POINT('Ctrl Pts',(-1.16619604579066,-5.43898472251395E-15,
-3.933825)) ;
#50116=CARTESIAN_POINT('Ctrl Pts',(-0.874647034342996,-0.504977700723842,
-3.88090833333333)) ;
#50117=CARTESIAN_POINT('Ctrl Pts',(-0.583098022895331,-1.00995540144768,
-3.82799166666667)) ;
#50118=CARTESIAN_POINT('Ctrl Pts',(-1.23683864966447E-16,-1.00995540144768,
-3.775075)) ;
#50119=CARTESIAN_POINT('Ctrl Pts',(0.58309802289533,-1.00995540144768,-3.72215833333333)) ;
#50120=CARTESIAN_POINT('Ctrl Pts',(0.874647034342996,-0.504977700723843,
-3.66924166666667)) ;
#50121=CARTESIAN_POINT('Ctrl Pts',(1.16619604579066,-5.72462037344511E-15,
-3.616325)) ;
#50122=CARTESIAN_POINT('Ctrl Pts',(0.874647034342997,0.504977700723831,
-3.56340833333334)) ;
#50123=CARTESIAN_POINT('Ctrl Pts',(0.583098022895331,1.00995540144767,-3.51049166666667)) ;
#50124=CARTESIAN_POINT('Ctrl Pts',(0.,1.00995540144767,-3.457575)) ;
#50125=CARTESIAN_POINT('Ctrl Pts',(-0.583098022895331,1.00995540144767,
-3.40465833333333)) ;
#50126=CARTESIAN_POINT('Ctrl Pts',(-0.874647034342996,0.504977700723831,
-3.35174166666667)) ;
#50127=CARTESIAN_POINT('Ctrl Pts',(-1.16619604579066,-5.43898472251395E-15,
-3.298825)) ;
#50128=CARTESIAN_POINT('Ctrl Pts',(-0.874647034342996,-0.504977700723842,
-3.24590833333334)) ;
#50129=CARTESIAN_POINT('Ctrl Pts',(-0.583098022895331,-1.00995540144768,
-3.19299166666667)) ;
#50130=CARTESIAN_POINT('Ctrl Pts',(-1.23683864966447E-16,-1.00995540144768,
-3.140075)) ;
#50131=CARTESIAN_POINT('Ctrl Pts',(0.58309802289533,-1.00995540144768,-3.08715833333333)) ;
#50132=CARTESIAN_POINT('Ctrl Pts',(0.874647034342996,-0.504977700723843,
-3.03424166666667)) ;
#50133=CARTESIAN_POINT('Ctrl Pts',(1.16619604579066,-5.72462037344511E-15,
-2.981325)) ;
#50134=CARTESIAN_POINT('Ctrl Pts',(0.874647034342997,0.504977700723831,
-2.92840833333333)) ;
#50135=CARTESIAN_POINT('Ctrl Pts',(0.583098022895331,1.00995540144767,-2.87549166666667)) ;
#50136=CARTESIAN_POINT('Ctrl Pts',(0.,1.00995540144767,-2.822575)) ;
#50137=CARTESIAN_POINT('Ctrl Pts',(-0.583098022895331,1.00995540144767,
-2.76965833333333)) ;
#50138=CARTESIAN_POINT('Ctrl Pts',(-0.874647034342996,0.504977700723831,
-2.71674166666667)) ;
#50139=CARTESIAN_POINT('Ctrl Pts',(-1.16619604579066,-5.43898472251395E-15,
-2.663825)) ;
#50140=CARTESIAN_POINT('Ctrl Pts',(-0.874647034342996,-0.504977700723842,
-2.61090833333333)) ;
#50141=CARTESIAN_POINT('Ctrl Pts',(-0.583098022895331,-1.00995540144768,
-2.55799166666667)) ;
#50142=CARTESIAN_POINT('Ctrl Pts',(-1.23683864966447E-16,-1.00995540144768,
-2.505075)) ;
#50143=CARTESIAN_POINT('Ctrl Pts',(0.58309802289533,-1.00995540144768,-2.45215833333333)) ;
#50144=CARTESIAN_POINT('Ctrl Pts',(0.874647034342996,-0.504977700723843,
-2.39924166666667)) ;
#50145=CARTESIAN_POINT('Ctrl Pts',(1.16619604579066,-5.72462037344511E-15,
-2.346325)) ;
#50146=CARTESIAN_POINT('Ctrl Pts',(0.874647034342997,0.504977700723831,
-2.29340833333333)) ;
#50147=CARTESIAN_POINT('Ctrl Pts',(0.583098022895331,1.00995540144767,-2.24049166666667)) ;
#50148=CARTESIAN_POINT('Ctrl Pts',(0.,1.00995540144767,-2.187575)) ;
#50149=CARTESIAN_POINT('Ctrl Pts',(-0.583098022895331,1.00995540144767,
-2.13465833333333)) ;
#50150=CARTESIAN_POINT('Ctrl Pts',(-0.874647034342996,0.504977700723831,
-2.08174166666667)) ;
#50151=CARTESIAN_POINT('Ctrl Pts',(-1.16619604579066,-5.43898472251395E-15,
-2.028825)) ;
#50152=CARTESIAN_POINT('Ctrl Pts',(-0.874647034342996,-0.504977700723842,
-1.97590833333333)) ;
#50153=CARTESIAN_POINT('Ctrl Pts',(-0.583098022895331,-1.00995540144768,
-1.92299166666667)) ;
#50154=CARTESIAN_POINT('Ctrl Pts',(-1.23683864966447E-16,-1.00995540144768,
-1.870075)) ;
#50155=CARTESIAN_POINT('Ctrl Pts',(0.58309802289533,-1.00995540144768,-1.81715833333333)) ;
#50156=CARTESIAN_POINT('Ctrl Pts',(0.874647034342996,-0.504977700723843,
-1.76424166666667)) ;
#50157=CARTESIAN_POINT('Ctrl Pts',(1.16619604579066,-5.72462037344511E-15,
-1.711325)) ;
#50158=CARTESIAN_POINT('Ctrl Pts',(0.874647034342997,0.504977700723831,
-1.65840833333333)) ;
#50159=CARTESIAN_POINT('Ctrl Pts',(0.583098022895331,1.00995540144767,-1.60549166666667)) ;
#50160=CARTESIAN_POINT('Ctrl Pts',(0.,1.00995540144767,-1.552575)) ;
#50161=CARTESIAN_POINT('Ctrl Pts',(-0.583098022895331,1.00995540144767,
-1.49965833333333)) ;
#50162=CARTESIAN_POINT('Ctrl Pts',(-0.874647034342996,0.504977700723831,
-1.44674166666667)) ;
#50163=CARTESIAN_POINT('Ctrl Pts',(-1.16619604579066,-5.43898472251395E-15,
-1.393825)) ;
#50164=CARTESIAN_POINT('Ctrl Pts',(-0.874647034342996,-0.504977700723842,
-1.34090833333333)) ;
#50165=CARTESIAN_POINT('Ctrl Pts',(-0.583098022895331,-1.00995540144768,
-1.28799166666667)) ;
#50166=CARTESIAN_POINT('Ctrl Pts',(-1.23683864966447E-16,-1.00995540144768,
-1.235075)) ;
#50167=CARTESIAN_POINT('Ctrl Pts',(0.58309802289533,-1.00995540144768,-1.18215833333333)) ;
#50168=CARTESIAN_POINT('Ctrl Pts',(0.874647034342996,-0.504977700723843,
-1.12924166666667)) ;
#50169=CARTESIAN_POINT('Ctrl Pts',(1.16619604579066,-5.72462037344511E-15,
-1.076325)) ;
#50170=CARTESIAN_POINT('Ctrl Pts',(0.874647034342997,0.504977700723831,
-1.02340833333333)) ;
#50171=CARTESIAN_POINT('Ctrl Pts',(0.583098022895331,1.00995540144767,-0.970491666666667)) ;
#50172=CARTESIAN_POINT('Ctrl Pts',(0.,1.00995540144767,-0.917575000000001)) ;
#50173=CARTESIAN_POINT('Ctrl Pts',(-0.583098022895331,1.00995540144767,
-0.864658333333334)) ;
#50174=CARTESIAN_POINT('Ctrl Pts',(-0.874647034342996,0.504977700723831,
-0.811741666666668)) ;
#50175=CARTESIAN_POINT('Ctrl Pts',(-1.16619604579066,-5.43898472251395E-15,
-0.758825000000001)) ;
#50176=CARTESIAN_POINT('Ctrl Pts',(-0.874647034342996,-0.504977700723842,
-0.705908333333334)) ;
#50177=CARTESIAN_POINT('Ctrl Pts',(-0.583098022895331,-1.00995540144768,
-0.652991666666667)) ;
#50178=CARTESIAN_POINT('Ctrl Pts',(-1.23683864966447E-16,-1.00995540144768,
-0.600075000000001)) ;
#50179=CARTESIAN_POINT('Ctrl Pts',(0.58309802289533,-1.00995540144768,-0.547158333333334)) ;
#50180=CARTESIAN_POINT('Ctrl Pts',(0.874647034342996,-0.504977700723843,
-0.494241666666667)) ;
#50181=CARTESIAN_POINT('Ctrl Pts',(1.16619604579066,-5.72462037344511E-15,
-0.441325000000001)) ;
#50182=CARTESIAN_POINT('Ctrl Pts',(0.874647034342997,0.504977700723831,
-0.388408333333334)) ;
#50183=CARTESIAN_POINT('Ctrl Pts',(0.583098022895331,1.00995540144767,-0.335491666666668)) ;
#50184=CARTESIAN_POINT('Ctrl Pts',(0.,1.00995540144767,-0.282575000000001)) ;
#50185=CARTESIAN_POINT('Ctrl Pts',(-0.583098022895331,1.00995540144767,
-0.229658333333334)) ;
#50186=CARTESIAN_POINT('Ctrl Pts',(-0.874647034342996,0.504977700723831,
-0.176741666666667)) ;
#50187=CARTESIAN_POINT('Ctrl Pts',(-1.16619604579066,-5.43898472251395E-15,
-0.123825000000001)) ;
#50188=CARTESIAN_POINT('Ctrl Pts',(-0.874647034342996,-0.504977700723842,
-0.0709083333333346)) ;
#50189=CARTESIAN_POINT('Ctrl Pts',(-0.583098022895331,-1.00995540144768,
-0.0179916666666674)) ;
#50190=CARTESIAN_POINT('Ctrl Pts',(-1.23683864966447E-16,-1.00995540144768,
0.034924999999999)) ;
#50191=CARTESIAN_POINT('Ctrl Pts',(0.58309802289533,-1.00995540144768,0.0878416666666654)) ;
#50192=CARTESIAN_POINT('Ctrl Pts',(0.874647034342996,-0.504977700723843,
0.140758333333333)) ;
#50193=CARTESIAN_POINT('Ctrl Pts',(1.16619604579066,-5.72462037344511E-15,
0.193674999999999)) ;
#50194=CARTESIAN_POINT('Ctrl Pts',(0.874647034342997,0.504977700723831,
0.246591666666665)) ;
#50195=CARTESIAN_POINT('Ctrl Pts',(0.583098022895331,1.00995540144767,0.299508333333333)) ;
#50196=CARTESIAN_POINT('Ctrl Pts',(0.,1.00995540144767,0.352424999999999)) ;
#50197=CARTESIAN_POINT('Ctrl Pts',(-0.583098022895331,1.00995540144767,
0.405341666666665)) ;
#50198=CARTESIAN_POINT('Ctrl Pts',(-0.874647034342996,0.504977700723831,
0.458258333333333)) ;
#50199=CARTESIAN_POINT('Ctrl Pts',(-1.16619604579066,-5.43898472251395E-15,
0.511174999999999)) ;
#50200=CARTESIAN_POINT('Ctrl Pts',(-0.874647034342996,-0.504977700723842,
0.564091666666666)) ;
#50201=CARTESIAN_POINT('Ctrl Pts',(-0.583098022895331,-1.00995540144768,
0.617008333333333)) ;
#50202=CARTESIAN_POINT('Ctrl Pts',(-1.23683864966447E-16,-1.00995540144768,
0.669924999999999)) ;
#50203=CARTESIAN_POINT('Ctrl Pts',(0.58309802289533,-1.00995540144768,0.722841666666665)) ;
#50204=CARTESIAN_POINT('Ctrl Pts',(0.874647034342996,-0.504977700723843,
0.775758333333332)) ;
#50205=CARTESIAN_POINT('Ctrl Pts',(1.16619604579066,-5.72462037344511E-15,
0.828674999999999)) ;
#50206=CARTESIAN_POINT('Ctrl Pts',(0.874647034342997,0.504977700723831,
0.881591666666666)) ;
#50207=CARTESIAN_POINT('Ctrl Pts',(0.583098022895331,1.00995540144767,0.934508333333332)) ;
#50208=CARTESIAN_POINT('Ctrl Pts',(0.,1.00995540144767,0.987424999999999)) ;
#50209=CARTESIAN_POINT('Ctrl Pts',(-0.583098022895331,1.00995540144767,
1.04034166666667)) ;
#50210=CARTESIAN_POINT('Ctrl Pts',(-0.874647034342996,0.504977700723831,
1.09325833333333)) ;
#50211=CARTESIAN_POINT('Ctrl Pts',(-1.16619604579066,-5.43898472251395E-15,
1.146175)) ;
#50212=CARTESIAN_POINT('Ctrl Pts',(-0.874647034342996,-0.504977700723842,
1.19909166666667)) ;
#50213=CARTESIAN_POINT('Ctrl Pts',(-0.583098022895331,-1.00995540144768,
1.25200833333333)) ;
#50214=CARTESIAN_POINT('Ctrl Pts',(-1.23683864966447E-16,-1.00995540144768,
1.304925)) ;
#50215=CARTESIAN_POINT('Ctrl Pts',(0.58309802289533,-1.00995540144768,1.35784166666667)) ;
#50216=CARTESIAN_POINT('Ctrl Pts',(0.874647034342996,-0.504977700723843,
1.41075833333333)) ;
#50217=CARTESIAN_POINT('Ctrl Pts',(1.00995540144771,-0.270616734209297,
1.43531704380105)) ;
#50218=CARTESIAN_POINT('Ctrl Pts',(1.00995540144767,1.30352329021787E-13,
1.46367500000001)) ;
#86286=UNCERTAINTY_MEASURE_WITH_UNIT(LENGTH_MEASURE(0.01),#86331,
'DISTANCE_ACCURACY_VALUE',
'Maximum model space distance between geometric entities at asserted c
onnectivities') ;
#86304=UNCERTAINTY_MEASURE_WITH_UNIT(LENGTH_MEASURE(0.01),#86331,
'DISTANCE_ACCURACY_VALUE',
'Maximum model space distance between geometric entities at asserted c
onnectivities') ;
#86312=(
GEOMETRIC_REPRESENTATION_CONTEXT(3)
GLOBAL_UNCERTAINTY_ASSIGNED_CONTEXT((#86286))
GLOBAL_UNIT_ASSIGNED_CONTEXT((#86331,#86333,#86334))
REPRESENTATION_CONTEXT('','3D')
) ;
#86330=(
GEOMETRIC_REPRESENTATION_CONTEXT(3)
GLOBAL_UNCERTAINTY_ASSIGNED_CONTEXT((#86304))
GLOBAL_UNIT_ASSIGNED_CONTEXT((#86331,#86333,#86334))
REPRESENTATION_CONTEXT('','3D')
) ;
#86331=(
LENGTH_UNIT()
NAMED_UNIT(*)
SI_UNIT(.MILLI.,.METRE.)
) ;
#86333=(
NAMED_UNIT(*)
PLANE_ANGLE_UNIT()
SI_UNIT($,.RADIAN.)
) ;
#86334=(
NAMED_UNIT(*)
SI_UNIT($,.STERADIAN.)
SOLID_ANGLE_UNIT()
) ;
#86342=SHAPE_DEFINITION_REPRESENTATION(#86372,#86458) ;
#86372=PRODUCT_DEFINITION_SHAPE('',$,#86484) ;
#86458=SHAPE_REPRESENTATION('',(#33124),#86312) ;
#86476=PRODUCT_DEFINITION_CONTEXT('part definition',#86553,'design') ;
#86484=PRODUCT_DEFINITION('Flat_Head_Screw','Flat_Head_Screw',#86509,#86476) ;
#86509=PRODUCT_DEFINITION_FORMATION('',$,#86562) ;
#86553=APPLICATION_CONTEXT(
'Core Data for Automotive Mechanical Design Process') ;
#86554=PRODUCT_CONTEXT('part definition',#86553,'mechanical') ;
#86562=PRODUCT('Flat_Head_Screw','Flat_Head_Screw',$,(#86554)) ;
#86582=PRESENTATION_STYLE_ASSIGNMENT((#86587)) ;
#86587=SURFACE_STYLE_USAGE(.BOTH.,#86592) ;
#86592=SURFACE_SIDE_STYLE('',(#86597)) ;
#86597=SURFACE_STYLE_FILL_AREA(#86602) ;
#86602=FILL_AREA_STYLE('Opaque(203,203,203)',(#86607)) ;
#86607=FILL_AREA_STYLE_COLOUR('Opaque(203,203,203)',#86612) ;
#86612=COLOUR_RGB('Opaque(203,203,203)', 0.66274510, 0.83137255, 0.94901961) ;
ENDSEC;
END-ISO-10303-21;
